ISO-10303-21;
HEADER;
FILE_DESCRIPTION (('STEP AP214'),
    '1' );
FILE_NAME ('Servo-Body.2.step',
    '2026-11-01T05:08:46',
    ( '' ),
    ( '' ),
    'SwSTEP 2.0',
    'SolidWorks 2024',
    '' );
FILE_SCHEMA (( 'AUTOMOTIVE_DESIGN' ));
ENDSEC;

DATA;
#5=EDGE_CURVE ( 'NONE', #7189, #2938, #55, .T. ) ;
#14=CARTESIAN_POINT ( 'NONE',  ( 36.99999999999999289, 6.000000000000000000, 17.99999999999998934 ) ) ;
#25=SHAPE_REPRESENTATION ( 'Servo-Body.2', ( #1488 ), #13563 ) ;
#29=DIRECTION ( 'NONE',  ( 0.000000000000000000, 1.000000000000000000, 0.000000000000000000 ) ) ;
#52=DIRECTION ( 'NONE',  ( 3.854941057726249930E-16, 0.000000000000000000, -1.000000000000000000 ) ) ;
#55=CIRCLE ( 'NONE', #10737, 4.000000000000000000 ) ;
#60=PLANE ( 'NONE',  #664 ) ;
#61=CARTESIAN_POINT ( 'NONE',  ( 35.99999999999999289, 10.00000000000000000, 17.99999999999998934 ) ) ;
#65=EDGE_CURVE ( 'NONE', #15220, #14044, #10978, .T. ) ;
#68=FACE_OUTER_BOUND ( 'NONE', #5126, .T. ) ;
#76=APPLICATION_CONTEXT ( 'automotive_design' ) ;
#83=CARTESIAN_POINT ( 'NONE',  ( -23.00000000000002487, 10.00000000000000000, -36.99999999999999289 ) ) ;
#87=ORIENTED_EDGE ( 'NONE', *, *, #7823, .T. ) ;
#93=ORIENTED_EDGE ( 'NONE', *, *, #501, .T. ) ;
#98=ORIENTED_EDGE ( 'NONE', *, *, #11496, .T. ) ;
#120=CIRCLE ( 'NONE', #5038, 4.000000000000007105 ) ;
#122=DIRECTION ( 'NONE',  ( 0.000000000000000000, 0.000000000000000000, 1.000000000000000000 ) ) ;
#127=ORIENTED_EDGE ( 'NONE', *, *, #13187, .F. ) ;
#131=DIRECTION ( 'NONE',  ( 0.000000000000000000, 0.000000000000000000, -1.000000000000000000 ) ) ;
#142=ORIENTED_EDGE ( 'NONE', *, *, #15134, .F. ) ;
#143=EDGE_CURVE ( 'NONE', #14752, #3203, #1424, .T. ) ;
#145=CARTESIAN_POINT ( 'NONE',  ( 39.99999999999999289, 10.00000000000000000, 26.00000000000000000 ) ) ;
#146=VECTOR ( 'NONE', #14491, 1000.000000000000000 ) ;
#153=LINE ( 'NONE', #237, #1917 ) ;
#168=CARTESIAN_POINT ( 'NONE',  ( -26.00000000000002132, 0.000000000000000000, 40.00000000000000711 ) ) ;
#181=ORIENTED_EDGE ( 'NONE', *, *, #15280, .F. ) ;
#205=DIRECTION ( 'NONE',  ( 0.000000000000000000, 0.000000000000000000, 1.000000000000000000 ) ) ;
#216=DIRECTION ( 'NONE',  ( -0.000000000000000000, -1.000000000000000000, -0.000000000000000000 ) ) ;
#221=VERTEX_POINT ( 'NONE', #7428 ) ;
#223=ORIENTED_EDGE ( 'NONE', *, *, #14861, .T. ) ;
#225=EDGE_CURVE ( 'NONE', #4912, #8178, #15786, .T. ) ;
#227=CARTESIAN_POINT ( 'NONE',  ( -23.00000000000002487, 10.00000000000000000, -36.99999999999999289 ) ) ;
#231=EDGE_CURVE ( 'NONE', #4632, #4912, #15094, .T. ) ;
#237=CARTESIAN_POINT ( 'NONE',  ( -22.00000000000001776, 10.00000000000000000, 33.00000000000000711 ) ) ;
#238=ORIENTED_EDGE ( 'NONE', *, *, #143, .T. ) ;
#243=DIRECTION ( 'NONE',  ( 0.000000000000000000, 1.000000000000000000, 0.000000000000000000 ) ) ;
#244=CARTESIAN_POINT ( 'NONE',  ( 30.99999999999997513, 10.00000000000000000, 30.99999999999999645 ) ) ;
#246=EDGE_LOOP ( 'NONE', ( #7986, #8833, #5081, #14451, #2592, #16759 ) ) ;
#249=CARTESIAN_POINT ( 'NONE',  ( 30.99999999999997868, 10.00000000000000000, -30.99999999999999645 ) ) ;
#255=LINE ( 'NONE', #13482, #2119 ) ;
#256=CARTESIAN_POINT ( 'NONE',  ( 22.99999999999998224, 10.00000000000000000, -31.00000000000003197 ) ) ;
#257=ORIENTED_EDGE ( 'NONE', *, *, #5085, .T. ) ;
#268=LINE ( 'NONE', #15969, #4523 ) ;
#281=EDGE_CURVE ( 'NONE', #13251, #11864, #11062, .T. ) ;
#295=VERTEX_POINT ( 'NONE', #5816 ) ;
#306=APPLICATION_CONTEXT ( 'automotive_design' ) ;
#321=ADVANCED_FACE ( 'NONE', ( #2203 ), #6061, .T. ) ;
#329=ORIENTED_EDGE ( 'NONE', *, *, #7062, .T. ) ;
#345=LINE ( 'NONE', #3090, #1996 ) ;
#352=VERTEX_POINT ( 'NONE', #4541 ) ;
#356=DIRECTION ( 'NONE',  ( 0.000000000000000000, -0.000000000000000000, 1.000000000000000000 ) ) ;
#367=VECTOR ( 'NONE', #10969, 1000.000000000000000 ) ;
#372=AXIS2_PLACEMENT_3D ( 'NONE', #13169, #29, #9227 ) ;
#378=AXIS2_PLACEMENT_3D ( 'NONE', #11973, #5431, #9391 ) ;
#380=CARTESIAN_POINT ( 'NONE',  ( -36.00000000000000711, 6.000000000000000000, -18.00000000000000355 ) ) ;
#397=CARTESIAN_POINT ( 'NONE',  ( -40.00000000000000711, 10.00000000000000000, -26.00000000000000000 ) ) ;
#413=ORIENTED_EDGE ( 'NONE', *, *, #3477, .T. ) ;
#417=DIRECTION ( 'NONE',  ( 0.000000000000000000, 1.000000000000000000, 0.000000000000000000 ) ) ;
#423=ORIENTED_EDGE ( 'NONE', *, *, #8704, .F. ) ;
#432=EDGE_LOOP ( 'NONE', ( #13764, #10573, #5104, #15752 ) ) ;
#463=EDGE_CURVE ( 'NONE', #12295, #11373, #4943, .T. ) ;
#477=EDGE_CURVE ( 'NONE', #14542, #2235, #14154, .T. ) ;
#482=ADVANCED_FACE ( 'NONE', ( #2373 ), #7600, .F. ) ;
#484=VECTOR ( 'NONE', #7409, 1000.000000000000000 ) ;
#488=LINE ( 'NONE', #145, #11605 ) ;
#491=LINE ( 'NONE', #13786, #10610 ) ;
#496=ORIENTED_EDGE ( 'NONE', *, *, #6783, .T. ) ;
#501=EDGE_CURVE ( 'NONE', #12090, #11379, #6820, .T. ) ;
#508=CARTESIAN_POINT ( 'NONE',  ( -26.00000000000002132, 10.00000000000000000, -39.99999999999999289 ) ) ;
#510=DIRECTION ( 'NONE',  ( -1.000000000000000000, 0.000000000000000000, -0.000000000000000000 ) ) ;
#511=CIRCLE ( 'NONE', #4877, 5.000000000000000888 ) ;
#514=CARTESIAN_POINT ( 'NONE',  ( 32.99999999999998579, 8.000000000000000000, 25.99999999999999645 ) ) ;
#525=ORIENTED_EDGE ( 'NONE', *, *, #3393, .T. ) ;
#529=VERTEX_POINT ( 'NONE', #13290 ) ;
#530=LINE ( 'NONE', #2063, #1767 ) ;
#547=EDGE_LOOP ( 'NONE', ( #8890, #8502, #7559, #15041 ) ) ;
#554=ORIENTED_EDGE ( 'NONE', *, *, #9518, .T. ) ;
#579=CARTESIAN_POINT ( 'NONE',  ( 39.99999999999999289, 8.000000000000000000, 18.99999999999999645 ) ) ;
#591=DIRECTION ( 'NONE',  ( -0.000000000000000000, -1.000000000000000000, -0.000000000000000000 ) ) ;
#593=CARTESIAN_POINT ( 'NONE',  ( 21.99999999999998224, 8.000000000000000000, -32.99999999999999289 ) ) ;
#594=VERTEX_POINT ( 'NONE', #5452 ) ;
#595=ADVANCED_FACE ( 'NONE', ( #8292 ), #10698, .F. ) ;
#611=EDGE_LOOP ( 'NONE', ( #7901, #9205, #87, #13240 ) ) ;
#613=VECTOR ( 'NONE', #417, 1000.000000000000000 ) ;
#621=EDGE_LOOP ( 'NONE', ( #15777, #12774, #1620, #6856, #2071, #9372 ) ) ;
#627=CARTESIAN_POINT ( 'NONE',  ( -26.00000000000001776, 8.000000000000000000, 33.00000000000000711 ) ) ;
#630=EDGE_LOOP ( 'NONE', ( #1582, #16288, #9962, #1330, #8933 ) ) ;
#647=DIRECTION ( 'NONE',  ( 0.000000000000000000, 0.000000000000000000, -1.000000000000000000 ) ) ;
#650=ORIENTED_EDGE ( 'NONE', *, *, #4882, .T. ) ;
#664=AXIS2_PLACEMENT_3D ( 'NONE', #15934, #9420, #9333 ) ;
#665=ADVANCED_FACE ( 'NONE', ( #1930, #12330 ), #8545, .T. ) ;
#667=FACE_OUTER_BOUND ( 'NONE', #15716, .T. ) ;
#694=ADVANCED_FACE ( 'NONE', ( #16525 ), #12663, .T. ) ;
#706=EDGE_LOOP ( 'NONE', ( #5585, #7438, #14987, #3458, #12125, #5109 ) ) ;
#708=VECTOR ( 'NONE', #10200, 1000.000000000000000 ) ;
#714=EDGE_CURVE ( 'NONE', #1311, #9832, #6041, .T. ) ;
#718=VECTOR ( 'NONE', #5173, 1000.000000000000000 ) ;
#725=ORIENTED_EDGE ( 'NONE', *, *, #12878, .F. ) ;
#729=AXIS2_PLACEMENT_3D ( 'NONE', #5206, #10459, #2640 ) ;
#730=ORIENTED_EDGE ( 'NONE', *, *, #13718, .F. ) ;
#740=VECTOR ( 'NONE', #2114, 1000.000000000000000 ) ;
#745=LINE ( 'NONE', #2016, #3137 ) ;
#751=ADVANCED_FACE ( 'NONE', ( #9922 ), #16366, .T. ) ;
#757=ORIENTED_EDGE ( 'NONE', *, *, #8896, .T. ) ;
#764=DIRECTION ( 'NONE',  ( -0.000000000000000000, -0.000000000000000000, 1.000000000000000000 ) ) ;
#776=DIRECTION ( 'NONE',  ( -0.000000000000000000, -0.000000000000000000, 1.000000000000000000 ) ) ;
#777=VERTEX_POINT ( 'NONE', #14211 ) ;
#778=CARTESIAN_POINT ( 'NONE',  ( 30.99999999999997513, 10.00000000000000000, 30.99999999999999645 ) ) ;
#780=DIRECTION ( 'NONE',  ( -0.000000000000000000, -1.000000000000000000, 0.000000000000000000 ) ) ;
#782=EDGE_CURVE ( 'NONE', #3745, #10488, #8803, .T. ) ;
#783=CARTESIAN_POINT ( 'NONE',  ( 31.00000000000001776, 10.00000000000000000, -25.99999999999999645 ) ) ;
#784=DIRECTION ( 'NONE',  ( 0.000000000000000000, 0.000000000000000000, -1.000000000000000000 ) ) ;
#787=EDGE_LOOP ( 'NONE', ( #12595, #7263, #98, #12446 ) ) ;
#788=LINE ( 'NONE', #3449, #2861 ) ;
#796=ORIENTED_EDGE ( 'NONE', *, *, #4563, .T. ) ;
#799=CARTESIAN_POINT ( 'NONE',  ( 25.99999999999997513, 10.00000000000000000, 31.00000000000003553 ) ) ;
#800=ORIENTED_EDGE ( 'NONE', *, *, #8558, .F. ) ;
#804=ORIENTED_EDGE ( 'NONE', *, *, #8582, .F. ) ;
#829=EDGE_CURVE ( 'NONE', #4632, #12051, #12754, .T. ) ;
#837=CIRCLE ( 'NONE', #10427, 4.000000000000003553 ) ;
#839=ORIENTED_EDGE ( 'NONE', *, *, #12634, .T. ) ;
#846=CARTESIAN_POINT ( 'NONE',  ( 35.99999999999999289, 10.00000000000000000, 18.99999999999999289 ) ) ;
#847=ORIENTED_EDGE ( 'NONE', *, *, #14322, .T. ) ;
#850=DIRECTION ( 'NONE',  ( 1.000000000000000000, 0.000000000000000000, 3.854941057726246479E-16 ) ) ;
#859=LINE ( 'NONE', #13995, #7290 ) ;
#860=ORIENTED_EDGE ( 'NONE', *, *, #6436, .T. ) ;
#878=ORIENTED_EDGE ( 'NONE', *, *, #6436, .F. ) ;
#886=VECTOR ( 'NONE', #12967, 1000.000000000000000 ) ;
#887=ORIENTED_EDGE ( 'NONE', *, *, #3842, .F. ) ;
#896=DIRECTION ( 'NONE',  ( 1.000000000000000000, 0.000000000000000000, 8.673617379884027583E-16 ) ) ;
#908=ORIENTED_EDGE ( 'NONE', *, *, #6783, .F. ) ;
#913=AXIS2_PLACEMENT_3D ( 'NONE', #4189, #11920, #14675 ) ;
#922=ORIENTED_EDGE ( 'NONE', *, *, #8662, .T. ) ;
#923=DIRECTION ( 'NONE',  ( -1.000000000000000000, 0.000000000000000000, -0.000000000000000000 ) ) ;
#932=CARTESIAN_POINT ( 'NONE',  ( -37.00000000000000711, 10.00000000000000000, -23.00000000000000000 ) ) ;
#933=VECTOR ( 'NONE', #1683, 1000.000000000000000 ) ;
#934=VECTOR ( 'NONE', #6013, 1000.000000000000000 ) ;
#935=LINE ( 'NONE', #11070, #3557 ) ;
#936=DIRECTION ( 'NONE',  ( 0.000000000000000000, 0.000000000000000000, -1.000000000000000000 ) ) ;
#941=CARTESIAN_POINT ( 'NONE',  ( 35.99999999999999289, 10.00000000000000000, 21.99999999999999645 ) ) ;
#950=LINE ( 'NONE', #2313, #2276 ) ;
#951=ORIENTED_EDGE ( 'NONE', *, *, #9601, .T. ) ;
#955=( LENGTH_UNIT ( ) NAMED_UNIT ( * ) SI_UNIT ( .MILLI., .METRE. ) );
#964=FACE_OUTER_BOUND ( 'NONE', #3481, .T. ) ;
#965=LINE ( 'NONE', #11513, #1254 ) ;
#969=VECTOR ( 'NONE', #13811, 1000.000000000000000 ) ;
#971=VERTEX_POINT ( 'NONE', #14636 ) ;
#998=EDGE_CURVE ( 'NONE', #9092, #5074, #1584, .T. ) ;
#1005=VECTOR ( 'NONE', #776, 1000.000000000000000 ) ;
#1007=DIRECTION ( 'NONE',  ( -0.000000000000000000, -1.000000000000000000, 0.000000000000000000 ) ) ;
#1028=CARTESIAN_POINT ( 'NONE',  ( 21.99999999999998224, 8.000000000000000000, -35.99999999999999289 ) ) ;
#1036=ORIENTED_EDGE ( 'NONE', *, *, #10885, .F. ) ;
#1056=AXIS2_PLACEMENT_3D ( 'NONE', #4958, #3776, #3522 ) ;
#1062=DIRECTION ( 'NONE',  ( 0.000000000000000000, 0.000000000000000000, 1.000000000000000000 ) ) ;
#1092=DIRECTION ( 'NONE',  ( 0.000000000000000000, 0.000000000000000000, -1.000000000000000000 ) ) ;
#1097=VECTOR ( 'NONE', #4107, 1000.000000000000000 ) ;
#1105=DIRECTION ( 'NONE',  ( 0.000000000000000000, 0.000000000000000000, 1.000000000000000000 ) ) ;
#1106=EDGE_CURVE ( 'NONE', #14016, #14542, #950, .T. ) ;
#1107=EDGE_CURVE ( 'NONE', #4162, #11680, #14076, .T. ) ;
#1110=CARTESIAN_POINT ( 'NONE',  ( 25.99999999999997868, 10.00000000000000000, 40.00000000000000711 ) ) ;
#1131=EDGE_LOOP ( 'NONE', ( #93, #3115, #16155, #1575 ) ) ;
#1145=VECTOR ( 'NONE', #9983, 1000.000000000000000 ) ;
#1148=DIRECTION ( 'NONE',  ( -1.000000000000000000, -0.000000000000000000, -0.000000000000000000 ) ) ;
#1156=VECTOR ( 'NONE', #14183, 1000.000000000000000 ) ;
#1158=CARTESIAN_POINT ( 'NONE',  ( -40.00000000000000711, 6.000000000000000000, -18.00000000000000355 ) ) ;
#1165=VECTOR ( 'NONE', #6571, 1000.000000000000000 ) ;
#1166=CARTESIAN_POINT ( 'NONE',  ( -33.00000000000000000, 8.000000000000000000, -26.00000000000000355 ) ) ;
#1167=PLANE ( 'NONE',  #9332 ) ;
#1170=CARTESIAN_POINT ( 'NONE',  ( 35.99999999999999289, 8.000000000000000000, 18.99999999999999289 ) ) ;
#1172=DIRECTION ( 'NONE',  ( 0.000000000000000000, -0.000000000000000000, 1.000000000000000000 ) ) ;
#1176=DIRECTION ( 'NONE',  ( 0.000000000000000000, 0.000000000000000000, -1.000000000000000000 ) ) ;
#1182=VECTOR ( 'NONE', #9131, 1000.000000000000000 ) ;
#1184=ORIENTED_EDGE ( 'NONE', *, *, #14322, .F. ) ;
#1187=DIRECTION ( 'NONE',  ( 0.000000000000000000, 0.000000000000000000, -1.000000000000000000 ) ) ;
#1192=CARTESIAN_POINT ( 'NONE',  ( -26.00000000000002132, 10.00000000000000000, 40.00000000000000711 ) ) ;
#1194=DIRECTION ( 'NONE',  ( 0.000000000000000000, 1.000000000000000000, 0.000000000000000000 ) ) ;
#1212=AXIS2_PLACEMENT_3D ( 'NONE', #778, #9719, #6164 ) ;
#1249=CARTESIAN_POINT ( 'NONE',  ( -31.00000000000005684, 0.000000000000000000, -23.00000000000000000 ) ) ;
#1254=VECTOR ( 'NONE', #4572, 1000.000000000000000 ) ;
#1263=ORIENTED_EDGE ( 'NONE', *, *, #8409, .F. ) ;
#1269=DIRECTION ( 'NONE',  ( -0.000000000000000000, 1.000000000000000000, -0.000000000000000000 ) ) ;
#1270=CARTESIAN_POINT ( 'NONE',  ( 25.99999999999998224, 6.000000000000000000, -31.99999999999998579 ) ) ;
#1272=DIRECTION ( 'NONE',  ( 0.000000000000000000, 0.000000000000000000, -1.000000000000000000 ) ) ;
#1299=VERTEX_POINT ( 'NONE', #256 ) ;
#1311=VERTEX_POINT ( 'NONE', #12018 ) ;
#1330=ORIENTED_EDGE ( 'NONE', *, *, #5308, .T. ) ;
#1339=VECTOR ( 'NONE', #16363, 1000.000000000000000 ) ;
#1371=ORIENTED_EDGE ( 'NONE', *, *, #16022, .T. ) ;
#1377=CARTESIAN_POINT ( 'NONE',  ( 31.99999999999998579, 10.00000000000000000, 21.99999999999999645 ) ) ;
#1379=VERTEX_POINT ( 'NONE', #12101 ) ;
#1380=VECTOR ( 'NONE', #8042, 1000.000000000000000 ) ;
#1406=PLANE ( 'NONE',  #6572 ) ;
#1408=DIRECTION ( 'NONE',  ( 0.000000000000000000, 1.000000000000000000, -0.000000000000000000 ) ) ;
#1424=CIRCLE ( 'NONE', #3885, 3.000000000000002665 ) ;
#1428=FACE_OUTER_BOUND ( 'NONE', #5494, .T. ) ;
#1429=VERTEX_POINT ( 'NONE', #14564 ) ;
#1434=VECTOR ( 'NONE', #7857, 1000.000000000000000 ) ;
#1436=CARTESIAN_POINT ( 'NONE',  ( -36.00000000000000711, 6.000000000000000000, -18.00000000000000355 ) ) ;
#1438=DIRECTION ( 'NONE',  ( 0.000000000000000000, 0.000000000000000000, -1.000000000000000000 ) ) ;
#1440=ORIENTED_EDGE ( 'NONE', *, *, #5741, .T. ) ;
#1450=LINE ( 'NONE', #11932, #6656 ) ;
#1451=AXIS2_PLACEMENT_3D ( 'NONE', #6157, #9956, #9795 ) ;
#1456=AXIS2_PLACEMENT_3D ( 'NONE', #8720, #3559, #8307 ) ;
#1488=AXIS2_PLACEMENT_3D ( 'NONE', #3280, #8693, #15217 ) ;
#1490=DIRECTION ( 'NONE',  ( -0.000000000000000000, -0.000000000000000000, -1.000000000000000000 ) ) ;
#1493=ORIENTED_EDGE ( 'NONE', *, *, #3119, .T. ) ;
#1497=CARTESIAN_POINT ( 'NONE',  ( -37.00000000000000711, 0.000000000000000000, 23.00000000000000000 ) ) ;
#1508=PLANE ( 'NONE',  #10751 ) ;
#1525=DIRECTION ( 'NONE',  ( 0.000000000000000000, 0.000000000000000000, -1.000000000000000000 ) ) ;
#1526=EDGE_CURVE ( 'NONE', #9900, #3550, #2708, .T. ) ;
#1527=LINE ( 'NONE', #12178, #613 ) ;
#1532=CARTESIAN_POINT ( 'NONE',  ( 25.99999999999997513, 0.000000000000000000, 31.00000000000003553 ) ) ;
#1543=ADVANCED_FACE ( 'NONE', ( #16358 ), #10953, .T. ) ;
#1546=EDGE_CURVE ( 'NONE', #16912, #12051, #2967, .T. ) ;
#1570=CIRCLE ( 'NONE', #11165, 4.000000000000003553 ) ;
#1575=ORIENTED_EDGE ( 'NONE', *, *, #3185, .T. ) ;
#1582=ORIENTED_EDGE ( 'NONE', *, *, #8753, .T. ) ;
#1584=LINE ( 'NONE', #4248, #7741 ) ;
#1585=ORIENTED_EDGE ( 'NONE', *, *, #5499, .T. ) ;
#1606=VERTEX_POINT ( 'NONE', #12247 ) ;
#1615=LINE ( 'NONE', #6834, #14730 ) ;
#1620=ORIENTED_EDGE ( 'NONE', *, *, #15280, .T. ) ;
#1625=DIRECTION ( 'NONE',  ( -0.000000000000000000, 1.000000000000000000, -0.000000000000000000 ) ) ;
#1640=CARTESIAN_POINT ( 'NONE',  ( -23.00000000000002487, 0.000000000000000000, -36.99999999999999289 ) ) ;
#1651=FACE_OUTER_BOUND ( 'NONE', #547, .T. ) ;
#1654=EDGE_CURVE ( 'NONE', #1299, #4138, #2093, .T. ) ;
#1661=ORIENTED_EDGE ( 'NONE', *, *, #1858, .T. ) ;
#1672=ORIENTED_EDGE ( 'NONE', *, *, #4289, .F. ) ;
#1678=VECTOR ( 'NONE', #10103, 1000.000000000000000 ) ;
#1683=DIRECTION ( 'NONE',  ( 0.000000000000000000, 0.000000000000000000, -1.000000000000000000 ) ) ;
#1732=DIRECTION ( 'NONE',  ( 0.000000000000000000, 0.000000000000000000, 1.000000000000000000 ) ) ;
#1745=VECTOR ( 'NONE', #16856, 1000.000000000000000 ) ;
#1748=CARTESIAN_POINT ( 'NONE',  ( 31.00000000000001776, 10.00000000000000000, -25.99999999999999645 ) ) ;
#1758=EDGE_LOOP ( 'NONE', ( #15888, #16873, #10157, #8053, #8499, #10175 ) ) ;
#1764=ADVANCED_FACE ( 'NONE', ( #7325 ), #15401, .T. ) ;
#1767=VECTOR ( 'NONE', #7199, 1000.000000000000000 ) ;
#1769=CARTESIAN_POINT ( 'NONE',  ( -40.00000000000000711, 6.000000000000000000, -18.00000000000000355 ) ) ;
#1784=ORIENTED_EDGE ( 'NONE', *, *, #11710, .T. ) ;
#1812=VERTEX_POINT ( 'NONE', #5411 ) ;
#1821=ORIENTED_EDGE ( 'NONE', *, *, #14733, .F. ) ;
#1828=ORIENTED_EDGE ( 'NONE', *, *, #5741, .F. ) ;
#1835=DIRECTION ( 'NONE',  ( -0.000000000000000000, -1.000000000000000000, -0.000000000000000000 ) ) ;
#1837=EDGE_CURVE ( 'NONE', #14282, #13693, #511, .T. ) ;
#1858=EDGE_CURVE ( 'NONE', #8348, #13693, #5487, .T. ) ;
#1864=ORIENTED_EDGE ( 'NONE', *, *, #5398, .T. ) ;
#1885=ORIENTED_EDGE ( 'NONE', *, *, #6312, .T. ) ;
#1889=FACE_OUTER_BOUND ( 'NONE', #14706, .T. ) ;
#1895=ORIENTED_EDGE ( 'NONE', *, *, #13793, .T. ) ;
#1911=VERTEX_POINT ( 'NONE', #1377 ) ;
#1912=ADVANCED_FACE ( 'NONE', ( #4048 ), #2932, .F. ) ;
#1913=EDGE_LOOP ( 'NONE', ( #2347, #2376, #16429, #15235 ) ) ;
#1916=EDGE_CURVE ( 'NONE', #14044, #11373, #9366, .T. ) ;
#1917=VECTOR ( 'NONE', #12260, 1000.000000000000000 ) ;
#1930=FACE_OUTER_BOUND ( 'NONE', #6718, .T. ) ;
#1936=ORIENTED_EDGE ( 'NONE', *, *, #5116, .T. ) ;
#1938=LINE ( 'NONE', #4928, #6715 ) ;
#1945=AXIS2_PLACEMENT_3D ( 'NONE', #5289, #15378, #3613 ) ;
#1947=LINE ( 'NONE', #508, #740 ) ;
#1948=VERTEX_POINT ( 'NONE', #3268 ) ;
#1953=CARTESIAN_POINT ( 'NONE',  ( 31.00000000000001421, 10.00000000000000000, 22.99999999999999645 ) ) ;
#1966=VECTOR ( 'NONE', #10588, 1000.000000000000000 ) ;
#1969=CYLINDRICAL_SURFACE ( 'NONE', #1212, 8.000000000000000000 ) ;
#1975=LINE ( 'NONE', #783, #15475 ) ;
#1977=VERTEX_POINT ( 'NONE', #3189 ) ;
#1984=AXIS2_PLACEMENT_3D ( 'NONE', #1158, #11386, #15418 ) ;
#1996=VECTOR ( 'NONE', #9358, 1000.000000000000000 ) ;
#2002=LINE ( 'NONE', #1769, #5254 ) ;
#2003=CARTESIAN_POINT ( 'NONE',  ( -23.00000000000002132, 6.000000000000000000, 32.00000000000000000 ) ) ;
#2016=CARTESIAN_POINT ( 'NONE',  ( 22.99999999999998224, 6.000000000000000000, -31.00000000000003197 ) ) ;
#2025=CARTESIAN_POINT ( 'NONE',  ( -32.00000000000000711, 6.000000000000000000, -23.00000000000000000 ) ) ;
#2039=LINE ( 'NONE', #5983, #7253 ) ;
#2055=DIRECTION ( 'NONE',  ( -0.000000000000000000, -1.000000000000000000, -0.000000000000000000 ) ) ;
#2063=CARTESIAN_POINT ( 'NONE',  ( -26.00000000000002132, 8.000000000000000000, 40.00000000000000711 ) ) ;
#2065=VERTEX_POINT ( 'NONE', #10049 ) ;
#2071=ORIENTED_EDGE ( 'NONE', *, *, #6201, .F. ) ;
#2086=CIRCLE ( 'NONE', #4557, 3.000000000000002665 ) ;
#2092=LINE ( 'NONE', #3473, #9439 ) ;
#2093=LINE ( 'NONE', #16517, #16944 ) ;
#2098=VECTOR ( 'NONE', #3498, 1000.000000000000000 ) ;
#2103=VERTEX_POINT ( 'NONE', #6077 ) ;
#2105=LINE ( 'NONE', #11133, #2328 ) ;
#2109=CARTESIAN_POINT ( 'NONE',  ( -19.00000000000001776, 8.000000000000000000, 40.00000000000000711 ) ) ;
#2110=CARTESIAN_POINT ( 'NONE',  ( -31.00000000000007105, 10.00000000000000000, 23.00000000000000000 ) ) ;
#2111=ORIENTED_EDGE ( 'NONE', *, *, #15800, .F. ) ;
#2114=DIRECTION ( 'NONE',  ( -1.000000000000000000, -0.000000000000000000, -0.000000000000000000 ) ) ;
#2119=VECTOR ( 'NONE', #14940, 1000.000000000000000 ) ;
#2120=CYLINDRICAL_SURFACE ( 'NONE', #4529, 4.000000000000003553 ) ;
#2125=ADVANCED_FACE ( 'NONE', ( #16809 ), #11666, .T. ) ;
#2135=FACE_OUTER_BOUND ( 'NONE', #12376, .T. ) ;
#2139=DIRECTION ( 'NONE',  ( -1.000000000000000000, -0.000000000000000000, 3.854941057726247958E-16 ) ) ;
#2142=VERTEX_POINT ( 'NONE', #13994 ) ;
#2149=EDGE_CURVE ( 'NONE', #529, #5229, #12793, .T. ) ;
#2177=PLANE ( 'NONE',  #3938 ) ;
#2200=FACE_OUTER_BOUND ( 'NONE', #246, .T. ) ;
#2201=VECTOR ( 'NONE', #2370, 1000.000000000000000 ) ;
#2203=FACE_OUTER_BOUND ( 'NONE', #787, .T. ) ;
#2205=LINE ( 'NONE', #10035, #3242 ) ;
#2207=DIRECTION ( 'NONE',  ( -0.000000000000000000, -0.000000000000000000, 1.000000000000000000 ) ) ;
#2226=DIRECTION ( 'NONE',  ( -0.000000000000000000, 1.000000000000000000, -0.000000000000000000 ) ) ;
#2235=VERTEX_POINT ( 'NONE', #12256 ) ;
#2259=AXIS2_PLACEMENT_3D ( 'NONE', #8392, #11287, #11375 ) ;
#2264=LINE ( 'NONE', #16770, #16105 ) ;
#2273=CIRCLE ( 'NONE', #1456, 7.999999999999996447 ) ;
#2274=DIRECTION ( 'NONE',  ( -3.854941057726253874E-16, 0.000000000000000000, -1.000000000000000000 ) ) ;
#2276=VECTOR ( 'NONE', #8935, 1000.000000000000000 ) ;
#2283=CIRCLE ( 'NONE', #10250, 7.999999999999996447 ) ;
#2310=ORIENTED_EDGE ( 'NONE', *, *, #13715, .T. ) ;
#2313=CARTESIAN_POINT ( 'NONE',  ( 39.99999999999999289, 8.000000000000000000, 18.99999999999999645 ) ) ;
#2318=SHAPE_REPRESENTATION_RELATIONSHIP ( 'NONE' , 'NONE' ,  #25, #7495 ) ;
#2322=LINE ( 'NONE', #5143, #5604 ) ;
#2328=VECTOR ( 'NONE', #3317, 1000.000000000000000 ) ;
#2333=ORIENTED_EDGE ( 'NONE', *, *, #5410, .F. ) ;
#2340=CARTESIAN_POINT ( 'NONE',  ( -23.00000000000002132, 10.00000000000000000, 31.00000000000003553 ) ) ;
#2346=DIRECTION ( 'NONE',  ( -0.000000000000000000, -1.000000000000000000, -0.000000000000000000 ) ) ;
#2347=ORIENTED_EDGE ( 'NONE', *, *, #8559, .T. ) ;
#2354=VERTEX_POINT ( 'NONE', #8289 ) ;
#2358=CARTESIAN_POINT ( 'NONE',  ( 17.99999999999998224, 10.00000000000000000, -36.99999999999999289 ) ) ;
#2364=EDGE_CURVE ( 'NONE', #16504, #10947, #6037, .T. ) ;
#2370=DIRECTION ( 'NONE',  ( 1.000000000000000000, 0.000000000000000000, 0.000000000000000000 ) ) ;
#2373=FACE_OUTER_BOUND ( 'NONE', #1913, .T. ) ;
#2376=ORIENTED_EDGE ( 'NONE', *, *, #13793, .F. ) ;
#2390=FACE_OUTER_BOUND ( 'NONE', #621, .T. ) ;
#2399=VECTOR ( 'NONE', #6152, 1000.000000000000000 ) ;
#2404=PLANE ( 'NONE',  #5201 ) ;
#2437=AXIS2_PLACEMENT_3D ( 'NONE', #13629, #11123, #6036 ) ;
#2441=PLANE ( 'NONE',  #12971 ) ;
#2446=LINE ( 'NONE', #15670, #6850 ) ;
#2452=LINE ( 'NONE', #6478, #12608 ) ;
#2454=VERTEX_POINT ( 'NONE', #8723 ) ;
#2458=CARTESIAN_POINT ( 'NONE',  ( -40.00000000000000711, 10.00000000000000000, 26.00000000000000000 ) ) ;
#2461=DIRECTION ( 'NONE',  ( -1.000000000000000000, 0.000000000000000000, 0.000000000000000000 ) ) ;
#2525=ORIENTED_EDGE ( 'NONE', *, *, #4192, .T. ) ;
#2528=FACE_OUTER_BOUND ( 'NONE', #611, .T. ) ;
#2532=VECTOR ( 'NONE', #13906, 1000.000000000000000 ) ;
#2537=CARTESIAN_POINT ( 'NONE',  ( 39.99999999999999289, 10.00000000000000000, 26.00000000000000000 ) ) ;
#2541=ORIENTED_EDGE ( 'NONE', *, *, #11717, .F. ) ;
#2542=ORIENTED_EDGE ( 'NONE', *, *, #14861, .F. ) ;
#2543=DIRECTION ( 'NONE',  ( 1.000000000000000000, -0.000000000000000000, 0.000000000000000000 ) ) ;
#2560=CIRCLE ( 'NONE', #11896, 8.000000000000000000 ) ;
#2565=LINE ( 'NONE', #16814, #16386 ) ;
#2580=AXIS2_PLACEMENT_3D ( 'NONE', #16476, #2055, #13992 ) ;
#2586=ADVANCED_FACE ( 'NONE', ( #9138 ), #8888, .T. ) ;
#2592=ORIENTED_EDGE ( 'NONE', *, *, #8046, .F. ) ;
#2620=FACE_OUTER_BOUND ( 'NONE', #10894, .T. ) ;
#2637=CARTESIAN_POINT ( 'NONE',  ( -22.00000000000001776, 6.000000000000000000, 32.00000000000000711 ) ) ;
#2640=DIRECTION ( 'NONE',  ( 0.000000000000000000, 0.000000000000000000, 1.000000000000000000 ) ) ;
#2641=ORIENTED_EDGE ( 'NONE', *, *, #16745, .T. ) ;
#2657=VECTOR ( 'NONE', #12498, 1000.000000000000000 ) ;
#2660=CARTESIAN_POINT ( 'NONE',  ( -19.00000000000001776, 8.000000000000000000, 36.00000000000000711 ) ) ;
#2662=VERTEX_POINT ( 'NONE', #380 ) ;
#2678=ADVANCED_FACE ( 'NONE', ( #13353 ), #4245, .T. ) ;
#2686=VECTOR ( 'NONE', #13454, 1000.000000000000000 ) ;
#2693=ORIENTED_EDGE ( 'NONE', *, *, #15802, .F. ) ;
#2698=LINE ( 'NONE', #3904, #718 ) ;
#2707=VERTEX_POINT ( 'NONE', #10677 ) ;
#2708=LINE ( 'NONE', #7936, #12132 ) ;
#2715=ORIENTED_EDGE ( 'NONE', *, *, #4289, .T. ) ;
#2723=DIRECTION ( 'NONE',  ( -0.000000000000000000, -1.000000000000000000, -0.000000000000000000 ) ) ;
#2745=LINE ( 'NONE', #2660, #8080 ) ;
#2746=CARTESIAN_POINT ( 'NONE',  ( 31.99999999999998579, 10.00000000000000000, 22.99999999999999645 ) ) ;
#2749=DIRECTION ( 'NONE',  ( 0.000000000000000000, 0.000000000000000000, -1.000000000000000000 ) ) ;
#2762=ORIENTED_EDGE ( 'NONE', *, *, #13411, .T. ) ;
#2766=ORIENTED_EDGE ( 'NONE', *, *, #11170, .T. ) ;
#2778=ORIENTED_EDGE ( 'NONE', *, *, #15679, .T. ) ;
#2783=PLANE ( 'NONE',  #4173 ) ;
#2790=CARTESIAN_POINT ( 'NONE',  ( -31.00000000000002132, 10.00000000000000000, -31.00000000000000000 ) ) ;
#2796=VECTOR ( 'NONE', #5655, 1000.000000000000000 ) ;
#2808=CYLINDRICAL_SURFACE ( 'NONE', #1945, 4.999999999999997335 ) ;
#2811=CARTESIAN_POINT ( 'NONE',  ( 36.99999999999999289, 10.00000000000000000, -22.99999999999999645 ) ) ;
#2839=CARTESIAN_POINT ( 'NONE',  ( -26.00000000000002132, 0.000000000000000000, -39.99999999999999289 ) ) ;
#2858=CARTESIAN_POINT ( 'NONE',  ( -40.00000000000000711, 0.000000000000000000, 26.00000000000000000 ) ) ;
#2861=VECTOR ( 'NONE', #2226, 1000.000000000000000 ) ;
#2885=CARTESIAN_POINT ( 'NONE',  ( -19.00000000000001776, 8.000000000000000000, 40.00000000000000711 ) ) ;
#2890=DIRECTION ( 'NONE',  ( -1.000000000000000000, 0.000000000000000000, 0.000000000000000000 ) ) ;
#2893=CARTESIAN_POINT ( 'NONE',  ( -23.00000000000002132, 0.000000000000000000, 31.00000000000003553 ) ) ;
#2905=AXIS2_PLACEMENT_3D ( 'NONE', #10829, #15880, #9363 ) ;
#2911=CARTESIAN_POINT ( 'NONE',  ( -36.00000000000000711, 10.00000000000000000, -22.00000000000000355 ) ) ;
#2912=EDGE_LOOP ( 'NONE', ( #12136, #951, #15678, #3160, #9853, #725 ) ) ;
#2913=CARTESIAN_POINT ( 'NONE',  ( 17.99999999999998579, 10.00000000000000000, -36.99999999999999289 ) ) ;
#2920=CARTESIAN_POINT ( 'NONE',  ( -26.00000000000001776, 0.000000000000000000, 31.00000000000003553 ) ) ;
#2930=VECTOR ( 'NONE', #10851, 1000.000000000000000 ) ;
#2932=PLANE ( 'NONE',  #15584 ) ;
#2934=EDGE_LOOP ( 'NONE', ( #8451, #11721, #14468, #7643 ) ) ;
#2938=VERTEX_POINT ( 'NONE', #9034 ) ;
#2945=CARTESIAN_POINT ( 'NONE',  ( -36.00000000000000711, 6.000000000000000000, -22.00000000000000355 ) ) ;
#2951=VECTOR ( 'NONE', #5250, 1000.000000000000000 ) ;
#2954=LINE ( 'NONE', #11791, #2951 ) ;
#2956=VERTEX_POINT ( 'NONE', #15476 ) ;
#2964=DIRECTION ( 'NONE',  ( 0.000000000000000000, 1.000000000000000000, 0.000000000000000000 ) ) ;
#2967=LINE ( 'NONE', #4427, #2686 ) ;
#2977=VERTEX_POINT ( 'NONE', #14 ) ;
#3015=VERTEX_POINT ( 'NONE', #12040 ) ;
#3020=ORIENTED_EDGE ( 'NONE', *, *, #11684, .T. ) ;
#3030=CARTESIAN_POINT ( 'NONE',  ( -31.00000000000005329, 0.000000000000000000, -26.00000000000000355 ) ) ;
#3032=VECTOR ( 'NONE', #9204, 1000.000000000000000 ) ;
#3033=ORIENTED_EDGE ( 'NONE', *, *, #6438, .F. ) ;
#3038=ORIENTED_EDGE ( 'NONE', *, *, #12545, .F. ) ;
#3043=VERTEX_POINT ( 'NONE', #6785 ) ;
#3070=DIRECTION ( 'NONE',  ( 3.854941057726258312E-16, -0.000000000000000000, 1.000000000000000000 ) ) ;
#3084=ORIENTED_EDGE ( 'NONE', *, *, #11492, .F. ) ;
#3087=AXIS2_PLACEMENT_3D ( 'NONE', #8489, #12519, #11309 ) ;
#3090=CARTESIAN_POINT ( 'NONE',  ( -26.00000000000002132, 10.00000000000000000, -31.00000000000003553 ) ) ;
#3092=EDGE_CURVE ( 'NONE', #15552, #9768, #530, .T. ) ;
#3105=ORIENTED_EDGE ( 'NONE', *, *, #4155, .F. ) ;
#3109=EDGE_CURVE ( 'NONE', #2235, #4506, #1975, .T. ) ;
#3115=ORIENTED_EDGE ( 'NONE', *, *, #6555, .F. ) ;
#3119=EDGE_CURVE ( 'NONE', #6145, #1948, #120, .T. ) ;
#3132=VECTOR ( 'NONE', #6636, 1000.000000000000000 ) ;
#3137=VECTOR ( 'NONE', #10960, 1000.000000000000000 ) ;
#3156=DIRECTION ( 'NONE',  ( 0.000000000000000000, 0.000000000000000000, -1.000000000000000000 ) ) ;
#3160=ORIENTED_EDGE ( 'NONE', *, *, #3490, .T. ) ;
#3162=CARTESIAN_POINT ( 'NONE',  ( 21.99999999999998224, 10.00000000000000000, -31.99999999999998579 ) ) ;
#3177=LINE ( 'NONE', #4692, #14125 ) ;
#3185=EDGE_CURVE ( 'NONE', #10548, #12090, #3194, .T. ) ;
#3189=CARTESIAN_POINT ( 'NONE',  ( 25.99999999999998224, 10.00000000000000000, -32.99999999999999289 ) ) ;
#3194=LINE ( 'NONE', #1110, #5763 ) ;
#3195=ORIENTED_EDGE ( 'NONE', *, *, #7394, .F. ) ;
#3200=ORIENTED_EDGE ( 'NONE', *, *, #6686, .T. ) ;
#3203=VERTEX_POINT ( 'NONE', #15368 ) ;
#3204=AXIS2_PLACEMENT_3D ( 'NONE', #1028, #6240, #11489 ) ;
#3210=DIRECTION ( 'NONE',  ( 1.000000000000000000, 0.000000000000000000, 0.000000000000000000 ) ) ;
#3214=ORIENTED_EDGE ( 'NONE', *, *, #3516, .T. ) ;
#3225=DIRECTION ( 'NONE',  ( 1.000000000000000000, 0.000000000000000000, 0.000000000000000000 ) ) ;
#3236=EDGE_CURVE ( 'NONE', #221, #971, #7122, .T. ) ;
#3242=VECTOR ( 'NONE', #12690, 1000.000000000000000 ) ;
#3249=LINE ( 'NONE', #5979, #2098 ) ;
#3255=DIRECTION ( 'NONE',  ( 0.000000000000000000, 0.000000000000000000, 1.000000000000000000 ) ) ;
#3256=LINE ( 'NONE', #1953, #8730 ) ;
#3264=EDGE_CURVE ( 'NONE', #9092, #11763, #3610, .T. ) ;
#3265=CARTESIAN_POINT ( 'NONE',  ( 35.99999999999999289, 6.000000000000000000, 17.99999999999998934 ) ) ;
#3266=EDGE_LOOP ( 'NONE', ( #14732, #9213, #9311, #1895 ) ) ;
#3268=CARTESIAN_POINT ( 'NONE',  ( 31.99999999999998579, 6.000000000000000000, 21.99999999999999645 ) ) ;
#3274=ORIENTED_EDGE ( 'NONE', *, *, #3092, .F. ) ;
#3276=LINE ( 'NONE', #9974, #9185 ) ;
#3280=CARTESIAN_POINT ( 'NONE',  ( 0.000000000000000000, 0.000000000000000000, 0.000000000000000000 ) ) ;
#3295=EDGE_CURVE ( 'NONE', #16003, #14137, #5471, .T. ) ;
#3304=EDGE_CURVE ( 'NONE', #15298, #6935, #4109, .T. ) ;
#3307=CARTESIAN_POINT ( 'NONE',  ( -40.00000000000000711, 0.000000000000000000, -26.00000000000000000 ) ) ;
#3310=LINE ( 'NONE', #8391, #8423 ) ;
#3317=DIRECTION ( 'NONE',  ( -1.000000000000000000, -0.000000000000000000, -8.673617379884027583E-16 ) ) ;
#3327=ORIENTED_EDGE ( 'NONE', *, *, #5874, .F. ) ;
#3342=EDGE_LOOP ( 'NONE', ( #4361, #796, #9751, #15593, #13311, #7898 ) ) ;
#3360=EDGE_LOOP ( 'NONE', ( #12084, #15318, #11221, #10300 ) ) ;
#3361=DIRECTION ( 'NONE',  ( -1.000000000000000000, 0.000000000000000000, -1.734723475976807094E-15 ) ) ;
#3368=CARTESIAN_POINT ( 'NONE',  ( 32.99999999999998579, 8.000000000000000000, 21.99999999999999645 ) ) ;
#3371=PLANE ( 'NONE',  #7475 ) ;
#3393=EDGE_CURVE ( 'NONE', #10548, #777, #1450, .T. ) ;
#3398=CARTESIAN_POINT ( 'NONE',  ( -18.00000000000001421, 6.000000000000000000, 40.00000000000000711 ) ) ;
#3413=CARTESIAN_POINT ( 'NONE',  ( 39.99999999999999289, 8.000000000000000000, 26.00000000000000000 ) ) ;
#3432=CARTESIAN_POINT ( 'NONE',  ( 32.99999999999998579, 8.000000000000000000, 25.99999999999999645 ) ) ;
#3448=ADVANCED_FACE ( 'NONE', ( #12277 ), #2120, .T. ) ;
#3449=CARTESIAN_POINT ( 'NONE',  ( -33.00000000000000000, 8.000000000000000000, -22.00000000000000355 ) ) ;
#3454=EDGE_LOOP ( 'NONE', ( #14871, #650, #16379, #3992, #1936 ) ) ;
#3458=ORIENTED_EDGE ( 'NONE', *, *, #225, .F. ) ;
#3467=CIRCLE ( 'NONE', #13067, 8.000000000000000000 ) ;
#3473=CARTESIAN_POINT ( 'NONE',  ( 35.99999999999999289, 6.000000000000000000, 17.99999999999998934 ) ) ;
#3476=LINE ( 'NONE', #11278, #13810 ) ;
#3477=EDGE_CURVE ( 'NONE', #16779, #4249, #12354, .T. ) ;
#3479=CARTESIAN_POINT ( 'NONE',  ( -23.00000000000002132, 10.00000000000000000, 37.00000000000000711 ) ) ;
#3481=EDGE_LOOP ( 'NONE', ( #9399, #9345, #16241, #6259 ) ) ;
#3485=ORIENTED_EDGE ( 'NONE', *, *, #3264, .T. ) ;
#3490=EDGE_CURVE ( 'NONE', #11680, #10468, #3177, .T. ) ;
#3498=DIRECTION ( 'NONE',  ( -1.000000000000000000, -0.000000000000000000, -0.000000000000000000 ) ) ;
#3502=CARTESIAN_POINT ( 'NONE',  ( -40.00000000000000711, 0.000000000000000000, 26.00000000000000000 ) ) ;
#3504=PLANE ( 'NONE',  #10551 ) ;
#3505=LINE ( 'NONE', #11312, #2399 ) ;
#3514=VECTOR ( 'NONE', #5227, 1000.000000000000000 ) ;
#3516=EDGE_CURVE ( 'NONE', #15290, #11828, #2039, .T. ) ;
#3519=EDGE_LOOP ( 'NONE', ( #3038, #9168, #3837, #14057 ) ) ;
#3522=DIRECTION ( 'NONE',  ( 0.000000000000000000, 0.000000000000000000, 1.000000000000000000 ) ) ;
#3533=ADVANCED_FACE ( 'NONE', ( #7522 ), #3504, .F. ) ;
#3535=ORIENTED_EDGE ( 'NONE', *, *, #16233, .F. ) ;
#3549=VECTOR ( 'NONE', #10260, 1000.000000000000000 ) ;
#3550=VERTEX_POINT ( 'NONE', #14310 ) ;
#3557=VECTOR ( 'NONE', #850, 1000.000000000000000 ) ;
#3559=DIRECTION ( 'NONE',  ( -0.000000000000000000, -1.000000000000000000, 0.000000000000000000 ) ) ;
#3564=ORIENTED_EDGE ( 'NONE', *, *, #9940, .T. ) ;
#3569=VERTEX_POINT ( 'NONE', #11556 ) ;
#3570=CARTESIAN_POINT ( 'NONE',  ( -40.00000000000000711, 8.000000000000000000, -26.00000000000000000 ) ) ;
#3574=PRESENTATION_STYLE_ASSIGNMENT (( #4855 ) ) ;
#3588=DIRECTION ( 'NONE',  ( -0.000000000000000000, -0.000000000000000000, 1.000000000000000000 ) ) ;
#3590=DIRECTION ( 'NONE',  ( 0.000000000000000000, 0.000000000000000000, -1.000000000000000000 ) ) ;
#3597=LINE ( 'NONE', #16803, #14887 ) ;
#3610=CIRCLE ( 'NONE', #7154, 8.000000000000000000 ) ;
#3611=ADVANCED_FACE ( 'NONE', ( #15350 ), #16551, .T. ) ;
#3612=( NAMED_UNIT ( * ) SI_UNIT ( $, .STERADIAN. ) SOLID_ANGLE_UNIT ( ) );
#3613=DIRECTION ( 'NONE',  ( 0.000000000000000000, 0.000000000000000000, -1.000000000000000000 ) ) ;
#3620=CARTESIAN_POINT ( 'NONE',  ( 22.99999999999998224, 10.00000000000000000, 37.00000000000000711 ) ) ;
#3630=DIRECTION ( 'NONE',  ( -0.000000000000000000, 1.000000000000000000, -0.000000000000000000 ) ) ;
#3634=EDGE_CURVE ( 'NONE', #10263, #1429, #15432, .T. ) ;
#3662=FILL_AREA_STYLE ('',( #15587 ) ) ;
#3671=DIRECTION ( 'NONE',  ( 0.000000000000000000, 0.000000000000000000, 1.000000000000000000 ) ) ;
#3675=AXIS2_PLACEMENT_3D ( 'NONE', #16437, #7147, #896 ) ;
#3678=CARTESIAN_POINT ( 'NONE',  ( -36.00000000000000711, 8.000000000000000000, -22.00000000000000355 ) ) ;
#3679=EDGE_LOOP ( 'NONE', ( #878, #8437, #3274, #10127, #7064, #7738 ) ) ;
#3680=CARTESIAN_POINT ( 'NONE',  ( 31.00000000000003553, 0.000000000000000000, -23.00000000000000000 ) ) ;
#3683=CARTESIAN_POINT ( 'NONE',  ( -36.00000000000000711, 10.00000000000000000, -19.00000000000000000 ) ) ;
#3686=CARTESIAN_POINT ( 'NONE',  ( -31.00000000000002132, 0.000000000000000000, -31.00000000000000000 ) ) ;
#3688=ORIENTED_EDGE ( 'NONE', *, *, #6555, .T. ) ;
#3696=LINE ( 'NONE', #8934, #11449 ) ;
#3698=ORIENTED_EDGE ( 'NONE', *, *, #15679, .F. ) ;
#3704=VECTOR ( 'NONE', #1625, 1000.000000000000000 ) ;
#3709=FACE_OUTER_BOUND ( 'NONE', #11271, .T. ) ;
#3716=VECTOR ( 'NONE', #15006, 1000.000000000000000 ) ;
#3717=VERTEX_POINT ( 'NONE', #10700 ) ;
#3724=ADVANCED_FACE ( 'NONE', ( #1428 ), #60, .F. ) ;
#3738=VERTEX_POINT ( 'NONE', #13032 ) ;
#3745=VERTEX_POINT ( 'NONE', #7945 ) ;
#3768=CARTESIAN_POINT ( 'NONE',  ( -19.00000000000001776, 8.000000000000000000, 40.00000000000000711 ) ) ;
#3769=CARTESIAN_POINT ( 'NONE',  ( 22.99999999999998224, 10.00000000000000000, 37.00000000000000711 ) ) ;
#3776=DIRECTION ( 'NONE',  ( 0.000000000000000000, 1.000000000000000000, 0.000000000000000000 ) ) ;
#3778=EDGE_LOOP ( 'NONE', ( #15568, #15227, #2541, #10921 ) ) ;
#3783=CARTESIAN_POINT ( 'NONE',  ( 36.99999999999999289, 10.00000000000000000, -22.99999999999999645 ) ) ;
#3802=EDGE_LOOP ( 'NONE', ( #423, #10749, #16222, #4761 ) ) ;
#3803=EDGE_CURVE ( 'NONE', #9900, #2103, #745, .T. ) ;
#3812=CARTESIAN_POINT ( 'NONE',  ( -23.00000000000002132, 10.00000000000000000, 37.00000000000000711 ) ) ;
#3837=ORIENTED_EDGE ( 'NONE', *, *, #10570, .T. ) ;
#3842=EDGE_CURVE ( 'NONE', #10263, #2977, #13464, .T. ) ;
#3867=CARTESIAN_POINT ( 'NONE',  ( -40.00000000000000711, 0.000000000000000000, 26.00000000000000000 ) ) ;
#3870=DIRECTION ( 'NONE',  ( 0.000000000000000000, 0.000000000000000000, -1.000000000000000000 ) ) ;
#3877=EDGE_LOOP ( 'NONE', ( #14895, #16664, #860, #525, #223, #2310, #9842, #4123, #13755, #4650, #6633, #3564, #5613, #12900, #14405, #7566, #8689, #16252, #9513, #9757, #11383, #13609, #11213, #4484, #16267, #1864, #13880, #7192 ) ) ;
#3885=AXIS2_PLACEMENT_3D ( 'NONE', #2911, #9530, #10636 ) ;
#3904=CARTESIAN_POINT ( 'NONE',  ( 30.99999999999997513, 10.00000000000000000, 25.99999999999999645 ) ) ;
#3908=ORIENTED_EDGE ( 'NONE', *, *, #10151, .T. ) ;
#3913=EDGE_CURVE ( 'NONE', #11935, #14137, #5799, .T. ) ;
#3938=AXIS2_PLACEMENT_3D ( 'NONE', #14993, #11370, #16606 ) ;
#3946=EDGE_CURVE ( 'NONE', #2956, #2142, #10327, .T. ) ;
#3960=VECTOR ( 'NONE', #15525, 1000.000000000000000 ) ;
#3964=CARTESIAN_POINT ( 'NONE',  ( -40.00000000000000711, 8.000000000000000000, -19.00000000000000355 ) ) ;
#3983=ORIENTED_EDGE ( 'NONE', *, *, #10885, .T. ) ;
#3989=CARTESIAN_POINT ( 'NONE',  ( -31.00000000000005329, 10.00000000000000000, -26.00000000000000355 ) ) ;
#3992=ORIENTED_EDGE ( 'NONE', *, *, #11613, .T. ) ;
#3995=ORIENTED_EDGE ( 'NONE', *, *, #714, .F. ) ;
#3998=CARTESIAN_POINT ( 'NONE',  ( -32.00000000000000711, 10.00000000000000000, -23.00000000000000000 ) ) ;
#4005=CARTESIAN_POINT ( 'NONE',  ( -23.00000000000002132, 10.00000000000000000, 31.00000000000003553 ) ) ;
#4006=VERTEX_POINT ( 'NONE', #11604 ) ;
#4019=VECTOR ( 'NONE', #15866, 1000.000000000000000 ) ;
#4021=VECTOR ( 'NONE', #1187, 1000.000000000000000 ) ;
#4025=ORIENTED_EDGE ( 'NONE', *, *, #3477, .F. ) ;
#4048=FACE_OUTER_BOUND ( 'NONE', #6027, .T. ) ;
#4049=DIRECTION ( 'NONE',  ( 0.000000000000000000, 0.000000000000000000, 1.000000000000000000 ) ) ;
#4067=EDGE_LOOP ( 'NONE', ( #2715, #5750, #10092, #3084 ) ) ;
#4073=ORIENTED_EDGE ( 'NONE', *, *, #1837, .T. ) ;
#4083=FACE_OUTER_BOUND ( 'NONE', #14220, .T. ) ;
#4097=LINE ( 'NONE', #5458, #12226 ) ;
#4101=CARTESIAN_POINT ( 'NONE',  ( 22.99999999999998224, 10.00000000000000000, 37.00000000000000711 ) ) ;
#4107=DIRECTION ( 'NONE',  ( -0.000000000000000000, -0.000000000000000000, 1.000000000000000000 ) ) ;
#4109=LINE ( 'NONE', #83, #6905 ) ;
#4123=ORIENTED_EDGE ( 'NONE', *, *, #3236, .F. ) ;
#4129=VECTOR ( 'NONE', #13781, 1000.000000000000000 ) ;
#4138=VERTEX_POINT ( 'NONE', #6865 ) ;
#4141=LINE ( 'NONE', #9301, #14667 ) ;
#4145=LINE ( 'NONE', #13171, #9246 ) ;
#4155=EDGE_CURVE ( 'NONE', #7960, #10824, #14528, .T. ) ;
#4158=ORIENTED_EDGE ( 'NONE', *, *, #6429, .F. ) ;
#4160=MECHANICAL_DESIGN_GEOMETRIC_PRESENTATION_REPRESENTATION('',(#10470),#12668);
#4162=VERTEX_POINT ( 'NONE', #10579 ) ;
#4169=DIRECTION ( 'NONE',  ( 0.000000000000000000, 0.000000000000000000, -1.000000000000000000 ) ) ;
#4173=AXIS2_PLACEMENT_3D ( 'NONE', #5529, #11804, #4259 ) ;
#4176=DIRECTION ( 'NONE',  ( 0.000000000000000000, 0.000000000000000000, -1.000000000000000000 ) ) ;
#4188=FACE_OUTER_BOUND ( 'NONE', #2912, .T. ) ;
#4189=CARTESIAN_POINT ( 'NONE',  ( 31.00000000000001776, 10.00000000000000000, -25.99999999999999645 ) ) ;
#4192=EDGE_CURVE ( 'NONE', #10633, #971, #10659, .T. ) ;
#4197=CARTESIAN_POINT ( 'NONE',  ( 21.99999999999998224, 8.000000000000000000, -32.99999999999999289 ) ) ;
#4220=ORIENTED_EDGE ( 'NONE', *, *, #13723, .F. ) ;
#4234=VERTEX_POINT ( 'NONE', #11336 ) ;
#4245=CYLINDRICAL_SURFACE ( 'NONE', #378, 4.000000000000007105 ) ;
#4248=CARTESIAN_POINT ( 'NONE',  ( 22.99999999999997513, 10.00000000000000000, 31.00000000000005684 ) ) ;
#4249=VERTEX_POINT ( 'NONE', #12626 ) ;
#4259=DIRECTION ( 'NONE',  ( 1.000000000000000000, 0.000000000000000000, -0.000000000000000000 ) ) ;
#4263=CARTESIAN_POINT ( 'NONE',  ( -19.00000000000001776, 10.00000000000000000, 40.00000000000000711 ) ) ;
#4267=EDGE_CURVE ( 'NONE', #16501, #3203, #788, .T. ) ;
#4289=EDGE_CURVE ( 'NONE', #14833, #10297, #3276, .T. ) ;
#4291=CARTESIAN_POINT ( 'NONE',  ( 31.99999999999998579, 6.000000000000000000, 25.99999999999999645 ) ) ;
#4324=VECTOR ( 'NONE', #1148, 1000.000000000000000 ) ;
#4349=CARTESIAN_POINT ( 'NONE',  ( -23.00000000000002842, 10.00000000000000000, -36.99999999999999289 ) ) ;
#4359=CARTESIAN_POINT ( 'NONE',  ( -23.00000000000002487, 6.000000000000000000, -36.99999999999999289 ) ) ;
#4361=ORIENTED_EDGE ( 'NONE', *, *, #7804, .F. ) ;
#4370=LINE ( 'NONE', #12092, #12797 ) ;
#4371=ORIENTED_EDGE ( 'NONE', *, *, #16642, .T. ) ;
#4384=EDGE_CURVE ( 'NONE', #11352, #295, #7543, .T. ) ;
#4385=CYLINDRICAL_SURFACE ( 'NONE', #8498, 2.999999999999995559 ) ;
#4388=ORIENTED_EDGE ( 'NONE', *, *, #6439, .F. ) ;
#4405=ORIENTED_EDGE ( 'NONE', *, *, #4904, .F. ) ;
#4427=CARTESIAN_POINT ( 'NONE',  ( -37.00000000000000711, 10.00000000000000000, -18.00000000000000355 ) ) ;
#4447=CARTESIAN_POINT ( 'NONE',  ( 22.99999999999998224, 0.000000000000000000, 37.00000000000000711 ) ) ;
#4466=DIRECTION ( 'NONE',  ( 0.000000000000000000, 0.000000000000000000, 1.000000000000000000 ) ) ;
#4484=ORIENTED_EDGE ( 'NONE', *, *, #13398, .T. ) ;
#4487=CARTESIAN_POINT ( 'NONE',  ( -22.00000000000001776, 10.00000000000000000, 32.00000000000000711 ) ) ;
#4506=VERTEX_POINT ( 'NONE', #11939 ) ;
#4516=PLANE ( 'NONE',  #3675 ) ;
#4523=VECTOR ( 'NONE', #10649, 1000.000000000000000 ) ;
#4525=ORIENTED_EDGE ( 'NONE', *, *, #3946, .T. ) ;
#4529=AXIS2_PLACEMENT_3D ( 'NONE', #7100, #7268, #3255 ) ;
#4539=VECTOR ( 'NONE', #1525, 1000.000000000000000 ) ;
#4541=CARTESIAN_POINT ( 'NONE',  ( 25.99999999999998224, 0.000000000000000000, -31.00000000000003197 ) ) ;
#4547=DIRECTION ( 'NONE',  ( 0.000000000000000000, 0.000000000000000000, 1.000000000000000000 ) ) ;
#4550=CARTESIAN_POINT ( 'NONE',  ( -40.00000000000000711, 0.000000000000000000, -26.00000000000000000 ) ) ;
#4557=AXIS2_PLACEMENT_3D ( 'NONE', #15693, #9182, #14416 ) ;
#4563=EDGE_CURVE ( 'NONE', #3015, #1977, #5312, .T. ) ;
#4572=DIRECTION ( 'NONE',  ( -1.000000000000000000, 0.000000000000000000, 0.000000000000000000 ) ) ;
#4580=EDGE_LOOP ( 'NONE', ( #16686, #7912, #14927, #5671 ) ) ;
#4585=ORIENTED_EDGE ( 'NONE', *, *, #13411, .F. ) ;
#4593=CARTESIAN_POINT ( 'NONE',  ( 32.99999999999998579, 8.000000000000000000, 25.99999999999999645 ) ) ;
#4594=FACE_OUTER_BOUND ( 'NONE', #6531, .T. ) ;
#4597=CARTESIAN_POINT ( 'NONE',  ( 25.99999999999998224, 8.000000000000000000, -32.99999999999999289 ) ) ;
#4603=AXIS2_PLACEMENT_3D ( 'NONE', #10115, #16635, #3590 ) ;
#4608=DIRECTION ( 'NONE',  ( -1.000000000000000000, 0.000000000000000000, 0.000000000000000000 ) ) ;
#4623=LINE ( 'NONE', #15197, #11051 ) ;
#4632=VERTEX_POINT ( 'NONE', #9273 ) ;
#4650=ORIENTED_EDGE ( 'NONE', *, *, #477, .T. ) ;
#4664=CARTESIAN_POINT ( 'NONE',  ( 31.00000000000001421, 0.000000000000000000, 25.99999999999999645 ) ) ;
#4686=CARTESIAN_POINT ( 'NONE',  ( 35.99999999999999289, 6.000000000000000000, 17.99999999999998934 ) ) ;
#4692=CARTESIAN_POINT ( 'NONE',  ( -31.00000000000005329, 10.00000000000000000, -26.00000000000000355 ) ) ;
#4693=CYLINDRICAL_SURFACE ( 'NONE', #4603, 8.000000000000000000 ) ;
#4697=CARTESIAN_POINT ( 'NONE',  ( -36.00000000000000711, 6.000000000000000000, -22.00000000000000355 ) ) ;
#4700=AXIS2_PLACEMENT_3D ( 'NONE', #3768, #9082, #1092 ) ;
#4705=CARTESIAN_POINT ( 'NONE',  ( -37.00000000000000711, 10.00000000000000000, 23.00000000000000000 ) ) ;
#4722=ORIENTED_EDGE ( 'NONE', *, *, #5842, .T. ) ;
#4741=EDGE_LOOP ( 'NONE', ( #11225, #4025, #7198, #2525 ) ) ;
#4755=DIRECTION ( 'NONE',  ( 0.000000000000000000, -0.000000000000000000, 1.000000000000000000 ) ) ;
#4761=ORIENTED_EDGE ( 'NONE', *, *, #1526, .F. ) ;
#4763=DIRECTION ( 'NONE',  ( 0.000000000000000000, 0.000000000000000000, 1.000000000000000000 ) ) ;
#4769=ADVANCED_FACE ( 'NONE', ( #12357 ), #7433, .F. ) ;
#4770=VECTOR ( 'NONE', #3630, 1000.000000000000000 ) ;
#4772=DIRECTION ( 'NONE',  ( 0.000000000000000000, 0.000000000000000000, 1.000000000000000000 ) ) ;
#4802=LINE ( 'NONE', #13830, #14381 ) ;
#4804=DIRECTION ( 'NONE',  ( -0.000000000000000000, 1.000000000000000000, -0.000000000000000000 ) ) ;
#4819=VECTOR ( 'NONE', #4763, 1000.000000000000000 ) ;
#4826=ORIENTED_EDGE ( 'NONE', *, *, #8155, .T. ) ;
#4836=LINE ( 'NONE', #2340, #10518 ) ;
#4842=CARTESIAN_POINT ( 'NONE',  ( -23.00000000000002132, 6.000000000000000000, 37.00000000000000711 ) ) ;
#4851=ORIENTED_EDGE ( 'NONE', *, *, #13718, .T. ) ;
#4855=SURFACE_STYLE_USAGE ( .BOTH. , #14390 ) ;
#4857=CARTESIAN_POINT ( 'NONE',  ( 39.99999999999999289, 10.00000000000000000, 26.00000000000000000 ) ) ;
#4864=CYLINDRICAL_SURFACE ( 'NONE', #10125, 3.000000000000002665 ) ;
#4877=AXIS2_PLACEMENT_3D ( 'NONE', #14788, #9460, #2749 ) ;
#4879=LINE ( 'NONE', #8928, #4021 ) ;
#4882=EDGE_CURVE ( 'NONE', #10633, #16779, #11655, .T. ) ;
#4889=DIRECTION ( 'NONE',  ( -0.000000000000000000, -1.000000000000000000, -0.000000000000000000 ) ) ;
#4901=LINE ( 'NONE', #627, #934 ) ;
#4904=EDGE_CURVE ( 'NONE', #7594, #14585, #8748, .T. ) ;
#4908=VERTEX_POINT ( 'NONE', #3680 ) ;
#4912=VERTEX_POINT ( 'NONE', #8921 ) ;
#4916=CARTESIAN_POINT ( 'NONE',  ( -32.00000000000000711, 6.000000000000000000, -22.00000000000000355 ) ) ;
#4928=CARTESIAN_POINT ( 'NONE',  ( 17.99999999999998224, 6.000000000000000000, -35.99999999999999289 ) ) ;
#4937=CIRCLE ( 'NONE', #16193, 2.999999999999995559 ) ;
#4943=LINE ( 'NONE', #15523, #15138 ) ;
#4955=DIRECTION ( 'NONE',  ( 0.000000000000000000, 0.000000000000000000, -1.000000000000000000 ) ) ;
#4956=ORIENTED_EDGE ( 'NONE', *, *, #5935, .F. ) ;
#4958=CARTESIAN_POINT ( 'NONE',  ( -22.00000000000001776, 6.000000000000000000, 36.00000000000000711 ) ) ;
#4968=CLOSED_SHELL ( 'NONE', ( #12804, #7182, #14843, #12480, #6095, #665, #15042, #14965, #595, #5629, #11135, #14427, #9521, #9735, #4769, #5953, #12396, #16444, #3533, #16812, #11427, #14616, #8584, #14199, #9347, #12942, #2586, #13401, #12975, #12004, #12434, #9906, #321, #9296, #3724, #14765, #3448, #1912, #751, #1543, #2125, #16559, #2678, #14238, #6045, #13276, #10556, #14127, #1764, #6042, #13002, #482, #14657, #3611, #13669, #13905, #15261, #10038, #6759, #16764, #9496, #694, #6003, #13388, #7367, #6019 ) ) ;
#4970=VECTOR ( 'NONE', #13930, 1000.000000000000000 ) ;
#4972=ORIENTED_EDGE ( 'NONE', *, *, #4155, .T. ) ;
#4976=CARTESIAN_POINT ( 'NONE',  ( 22.99999999999998224, 0.000000000000000000, 37.00000000000000711 ) ) ;
#4980=CARTESIAN_POINT ( 'NONE',  ( -36.00000000000000711, 8.000000000000000000, -22.00000000000000355 ) ) ;
#5002=CARTESIAN_POINT ( 'NONE',  ( -40.00000000000000711, 10.00000000000000000, 26.00000000000000000 ) ) ;
#5016=CIRCLE ( 'NONE', #12176, 8.000000000000000000 ) ;
#5029=DIRECTION ( 'NONE',  ( 0.000000000000000000, 1.000000000000000000, 0.000000000000000000 ) ) ;
#5038=AXIS2_PLACEMENT_3D ( 'NONE', #15112, #14958, #7369 ) ;
#5047=VECTOR ( 'NONE', #5138, 1000.000000000000000 ) ;
#5055=VERTEX_POINT ( 'NONE', #2893 ) ;
#5074=VERTEX_POINT ( 'NONE', #8133 ) ;
#5075=EDGE_CURVE ( 'NONE', #10297, #11828, #4097, .T. ) ;
#5077=ORIENTED_EDGE ( 'NONE', *, *, #225, .T. ) ;
#5081=ORIENTED_EDGE ( 'NONE', *, *, #14921, .T. ) ;
#5085=EDGE_CURVE ( 'NONE', #1429, #295, #5283, .T. ) ;
#5086=ORIENTED_EDGE ( 'NONE', *, *, #8643, .F. ) ;
#5091=EDGE_LOOP ( 'NONE', ( #13877, #4525, #2111, #1661, #1784, #7314 ) ) ;
#5093=DIRECTION ( 'NONE',  ( 1.000000000000000000, -0.000000000000000000, 0.000000000000000000 ) ) ;
#5102=DIRECTION ( 'NONE',  ( 0.000000000000000000, 1.000000000000000000, 0.000000000000000000 ) ) ;
#5103=ORIENTED_EDGE ( 'NONE', *, *, #3516, .F. ) ;
#5104=ORIENTED_EDGE ( 'NONE', *, *, #14644, .T. ) ;
#5109=ORIENTED_EDGE ( 'NONE', *, *, #829, .T. ) ;
#5110=VECTOR ( 'NONE', #1835, 1000.000000000000000 ) ;
#5112=PLANE ( 'NONE',  #9714 ) ;
#5116=EDGE_CURVE ( 'NONE', #14016, #6668, #2105, .T. ) ;
#5126=EDGE_LOOP ( 'NONE', ( #14085, #8757, #4956, #6794 ) ) ;
#5130=VERTEX_POINT ( 'NONE', #12587 ) ;
#5135=DIRECTION ( 'NONE',  ( 0.000000000000000000, 0.000000000000000000, -1.000000000000000000 ) ) ;
#5138=DIRECTION ( 'NONE',  ( -0.000000000000000000, -1.000000000000000000, -0.000000000000000000 ) ) ;
#5143=CARTESIAN_POINT ( 'NONE',  ( -22.00000000000001776, 8.000000000000000000, 33.00000000000000711 ) ) ;
#5164=LINE ( 'NONE', #10416, #14898 ) ;
#5165=CARTESIAN_POINT ( 'NONE',  ( 22.99999999999998224, 10.00000000000000000, -36.99999999999999289 ) ) ;
#5173=DIRECTION ( 'NONE',  ( -0.000000000000000000, -1.000000000000000000, -0.000000000000000000 ) ) ;
#5175=ORIENTED_EDGE ( 'NONE', *, *, #4904, .T. ) ;
#5176=CIRCLE ( 'NONE', #15349, 4.000000000000000000 ) ;
#5178=PLANE ( 'NONE',  #7420 ) ;
#5180=CARTESIAN_POINT ( 'NONE',  ( 17.99999999999998224, 6.000000000000000000, -35.99999999999999289 ) ) ;
#5187=CARTESIAN_POINT ( 'NONE',  ( -31.00000000000005684, 10.00000000000000000, -23.00000000000000000 ) ) ;
#5193=ORIENTED_EDGE ( 'NONE', *, *, #4267, .F. ) ;
#5199=DIRECTION ( 'NONE',  ( 0.000000000000000000, 0.000000000000000000, -1.000000000000000000 ) ) ;
#5201=AXIS2_PLACEMENT_3D ( 'NONE', #8852, #10455, #10626 ) ;
#5204=EDGE_CURVE ( 'NONE', #2454, #4908, #14918, .T. ) ;
#5206=CARTESIAN_POINT ( 'NONE',  ( 21.99999999999998224, 8.000000000000000000, -35.99999999999999289 ) ) ;
#5219=DIRECTION ( 'NONE',  ( 1.000000000000000000, -0.000000000000000000, 3.854941057726254860E-16 ) ) ;
#5223=AXIS2_PLACEMENT_3D ( 'NONE', #5263, #6466, #9242 ) ;
#5224=DIRECTION ( 'NONE',  ( 0.000000000000000000, 0.000000000000000000, 1.000000000000000000 ) ) ;
#5227=DIRECTION ( 'NONE',  ( -0.000000000000000000, -1.000000000000000000, -0.000000000000000000 ) ) ;
#5229=VERTEX_POINT ( 'NONE', #3162 ) ;
#5234=ORIENTED_EDGE ( 'NONE', *, *, #5, .T. ) ;
#5247=EDGE_CURVE ( 'NONE', #5278, #11935, #1938, .T. ) ;
#5250=DIRECTION ( 'NONE',  ( -0.000000000000000000, 1.000000000000000000, -0.000000000000000000 ) ) ;
#5254=VECTOR ( 'NONE', #3225, 1000.000000000000000 ) ;
#5258=DIRECTION ( 'NONE',  ( -0.000000000000000000, -1.000000000000000000, -0.000000000000000000 ) ) ;
#5260=AXIS2_PLACEMENT_3D ( 'NONE', #3686, #16890, #15612 ) ;
#5263=CARTESIAN_POINT ( 'NONE',  ( 30.99999999999997868, 10.00000000000000000, -30.99999999999999645 ) ) ;
#5264=DIRECTION ( 'NONE',  ( 0.000000000000000000, 0.000000000000000000, -1.000000000000000000 ) ) ;
#5269=DIRECTION ( 'NONE',  ( 1.000000000000000000, -0.000000000000000000, 3.854941057726249930E-16 ) ) ;
#5278=VERTEX_POINT ( 'NONE', #12917 ) ;
#5283=LINE ( 'NONE', #9337, #4539 ) ;
#5289=CARTESIAN_POINT ( 'NONE',  ( -31.00000000000002132, 10.00000000000000000, -31.00000000000000000 ) ) ;
#5296=FACE_OUTER_BOUND ( 'NONE', #3877, .T. ) ;
#5300=VECTOR ( 'NONE', #12825, 1000.000000000000000 ) ;
#5301=DIRECTION ( 'NONE',  ( -0.000000000000000000, -1.000000000000000000, -0.000000000000000000 ) ) ;
#5308=EDGE_CURVE ( 'NONE', #10947, #9234, #16866, .T. ) ;
#5311=EDGE_CURVE ( 'NONE', #352, #14044, #12759, .T. ) ;
#5312=LINE ( 'NONE', #7968, #3704 ) ;
#5354=EDGE_CURVE ( 'NONE', #14978, #352, #7663, .T. ) ;
#5356=EDGE_LOOP ( 'NONE', ( #12269, #3020, #13352, #14960, #11921, #10629 ) ) ;
#5365=DIRECTION ( 'NONE',  ( -1.000000000000000000, 0.000000000000000000, 0.000000000000000000 ) ) ;
#5369=CIRCLE ( 'NONE', #10863, 5.000000000000000888 ) ;
#5371=CARTESIAN_POINT ( 'NONE',  ( 25.99999999999997868, 0.000000000000000000, 40.00000000000000711 ) ) ;
#5375=ORIENTED_EDGE ( 'NONE', *, *, #14643, .F. ) ;
#5376=DIRECTION ( 'NONE',  ( 0.000000000000000000, 1.000000000000000000, 0.000000000000000000 ) ) ;
#5386=FACE_OUTER_BOUND ( 'NONE', #4580, .T. ) ;
#5392=VECTOR ( 'NONE', #3210, 1000.000000000000000 ) ;
#5398=EDGE_CURVE ( 'NONE', #1379, #8348, #5369, .T. ) ;
#5399=LINE ( 'NONE', #11679, #886 ) ;
#5400=VECTOR ( 'NONE', #784, 1000.000000000000000 ) ;
#5408=EDGE_LOOP ( 'NONE', ( #10024, #15896, #13748, #5077, #10210, #6021, #10564, #12791, #9643, #1885, #4851, #257, #12671, #16494, #16816, #16693 ) ) ;
#5410=EDGE_CURVE ( 'NONE', #15604, #7379, #2698, .T. ) ;
#5411=CARTESIAN_POINT ( 'NONE',  ( -18.00000000000001421, 10.00000000000000000, 36.00000000000000711 ) ) ;
#5416=ORIENTED_EDGE ( 'NONE', *, *, #8895, .F. ) ;
#5417=CARTESIAN_POINT ( 'NONE',  ( 18.99999999999998224, 8.000000000000000000, -39.99999999999999289 ) ) ;
#5422=CARTESIAN_POINT ( 'NONE',  ( -22.00000000000001776, 6.000000000000000000, 36.00000000000000711 ) ) ;
#5431=DIRECTION ( 'NONE',  ( 0.000000000000000000, 1.000000000000000000, 0.000000000000000000 ) ) ;
#5432=ORIENTED_EDGE ( 'NONE', *, *, #11496, .F. ) ;
#5452=CARTESIAN_POINT ( 'NONE',  ( 39.99999999999999289, 0.000000000000000000, 26.00000000000000000 ) ) ;
#5458=CARTESIAN_POINT ( 'NONE',  ( -23.00000000000002132, 10.00000000000000000, 32.00000000000000711 ) ) ;
#5468=DIRECTION ( 'NONE',  ( -0.000000000000000000, 0.000000000000000000, 1.000000000000000000 ) ) ;
#5471=LINE ( 'NONE', #2913, #12943 ) ;
#5487=LINE ( 'NONE', #10734, #3514 ) ;
#5494=EDGE_LOOP ( 'NONE', ( #13010, #142, #15634, #14020 ) ) ;
#5499=EDGE_CURVE ( 'NONE', #9832, #14585, #15750, .T. ) ;
#5509=DIRECTION ( 'NONE',  ( -0.000000000000000000, -1.000000000000000000, 0.000000000000000000 ) ) ;
#5516=EDGE_LOOP ( 'NONE', ( #8047, #1585, #10554, #2693 ) ) ;
#5529=CARTESIAN_POINT ( 'NONE',  ( 35.99999999999999289, 6.000000000000000000, 17.99999999999998934 ) ) ;
#5539=AXIS2_PLACEMENT_3D ( 'NONE', #10083, #5219, #7971 ) ;
#5541=CARTESIAN_POINT ( 'NONE',  ( 30.99999999999997868, 10.00000000000000000, -30.99999999999999645 ) ) ;
#5545=VERTEX_POINT ( 'NONE', #7061 ) ;
#5556=VECTOR ( 'NONE', #15026, 1000.000000000000000 ) ;
#5573=CARTESIAN_POINT ( 'NONE',  ( 31.00000000000001421, 10.00000000000000000, 22.99999999999999645 ) ) ;
#5584=LINE ( 'NONE', #9722, #10052 ) ;
#5585=ORIENTED_EDGE ( 'NONE', *, *, #1546, .F. ) ;
#5593=VECTOR ( 'NONE', #11452, 1000.000000000000000 ) ;
#5599=DIRECTION ( 'NONE',  ( 0.000000000000000000, 1.000000000000000000, 0.000000000000000000 ) ) ;
#5604=VECTOR ( 'NONE', #8699, 1000.000000000000000 ) ;
#5613=ORIENTED_EDGE ( 'NONE', *, *, #10628, .T. ) ;
#5624=DIRECTION ( 'NONE',  ( -1.000000000000000000, -0.000000000000000000, -0.000000000000000000 ) ) ;
#5627=DIRECTION ( 'NONE',  ( -0.000000000000000000, -1.000000000000000000, 0.000000000000000000 ) ) ;
#5629=ADVANCED_FACE ( 'NONE', ( #8164 ), #9545, .F. ) ;
#5640=VERTEX_POINT ( 'NONE', #2746 ) ;
#5646=ORIENTED_EDGE ( 'NONE', *, *, #5410, .T. ) ;
#5648=CARTESIAN_POINT ( 'NONE',  ( -26.00000000000002132, 0.000000000000000000, -39.99999999999999289 ) ) ;
#5650=PLANE ( 'NONE',  #14161 ) ;
#5655=DIRECTION ( 'NONE',  ( -0.000000000000000000, -1.000000000000000000, -0.000000000000000000 ) ) ;
#5671=ORIENTED_EDGE ( 'NONE', *, *, #8352, .F. ) ;
#5676=ORIENTED_EDGE ( 'NONE', *, *, #3304, .F. ) ;
#5687=CYLINDRICAL_SURFACE ( 'NONE', #11023, 4.000000000000000000 ) ;
#5698=EDGE_LOOP ( 'NONE', ( #7805, #8737, #5234, #8175, #4405, #7129, #14882, #181, #8773, #496, #6491, #14406, #5432, #15743, #15309, #3698, #4722, #3327, #14876, #14112, #1821, #6545, #10249, #6912, #16424, #5103, #8614, #15574 ) ) ;
#5706=VERTEX_POINT ( 'NONE', #13234 ) ;
#5713=PLANE ( 'NONE',  #2437 ) ;
#5721=ORIENTED_EDGE ( 'NONE', *, *, #11694, .T. ) ;
#5723=CARTESIAN_POINT ( 'NONE',  ( 31.00000000000003553, 10.00000000000000000, -23.00000000000000000 ) ) ;
#5727=EDGE_CURVE ( 'NONE', #16912, #2707, #10650, .T. ) ;
#5729=DIRECTION ( 'NONE',  ( -0.000000000000000000, -1.000000000000000000, 0.000000000000000000 ) ) ;
#5736=AXIS2_PLACEMENT_3D ( 'NONE', #3479, #13956, #6121 ) ;
#5741=EDGE_CURVE ( 'NONE', #6145, #8810, #7361, .T. ) ;
#5745=DIRECTION ( 'NONE',  ( -0.000000000000000000, -1.000000000000000000, -0.000000000000000000 ) ) ;
#5750=ORIENTED_EDGE ( 'NONE', *, *, #5075, .T. ) ;
#5760=AXIS2_PLACEMENT_3D ( 'NONE', #8995, #14227, #16790 ) ;
#5763=VECTOR ( 'NONE', #4889, 1000.000000000000000 ) ;
#5772=CARTESIAN_POINT ( 'NONE',  ( -31.00000000000002132, 0.000000000000000000, -31.00000000000000000 ) ) ;
#5774=ORIENTED_EDGE ( 'NONE', *, *, #8752, .T. ) ;
#5785=ORIENTED_EDGE ( 'NONE', *, *, #998, .F. ) ;
#5799=LINE ( 'NONE', #16285, #7776 ) ;
#5816=CARTESIAN_POINT ( 'NONE',  ( 36.99999999999999289, 0.000000000000000000, -22.99999999999999645 ) ) ;
#5821=EDGE_LOOP ( 'NONE', ( #12391, #14163, #16528, #8112 ) ) ;
#5831=LINE ( 'NONE', #16723, #14441 ) ;
#5842=EDGE_CURVE ( 'NONE', #8810, #1911, #10600, .T. ) ;
#5844=EDGE_LOOP ( 'NONE', ( #4585, #1672, #14698, #4158, #11178 ) ) ;
#5867=CIRCLE ( 'NONE', #12458, 3.999999999999996447 ) ;
#5874=EDGE_CURVE ( 'NONE', #5640, #1911, #5831, .T. ) ;
#5879=DIRECTION ( 'NONE',  ( 1.000000000000000000, 0.000000000000000000, 0.000000000000000000 ) ) ;
#5886=DIRECTION ( 'NONE',  ( 0.000000000000000000, 0.000000000000000000, -1.000000000000000000 ) ) ;
#5935=EDGE_CURVE ( 'NONE', #9768, #5545, #4879, .T. ) ;
#5945=ORIENTED_EDGE ( 'NONE', *, *, #4563, .F. ) ;
#5953=ADVANCED_FACE ( 'NONE', ( #11663 ), #14325, .F. ) ;
#5978=DIRECTION ( 'NONE',  ( 0.000000000000000000, 0.000000000000000000, 1.000000000000000000 ) ) ;
#5979=CARTESIAN_POINT ( 'NONE',  ( -23.00000000000002487, 0.000000000000000000, -36.99999999999999289 ) ) ;
#5983=CARTESIAN_POINT ( 'NONE',  ( -23.00000000000002132, 10.00000000000000000, 37.00000000000000711 ) ) ;
#5988=ORIENTED_EDGE ( 'NONE', *, *, #10444, .F. ) ;
#6003=ADVANCED_FACE ( 'NONE', ( #9011 ), #8377, .F. ) ;
#6011=EDGE_CURVE ( 'NONE', #6668, #10633, #2086, .T. ) ;
#6013=DIRECTION ( 'NONE',  ( -4.956352788505164254E-16, 0.000000000000000000, 1.000000000000000000 ) ) ;
#6019=ADVANCED_FACE ( 'NONE', ( #14073 ), #7533, .T. ) ;
#6021=ORIENTED_EDGE ( 'NONE', *, *, #15506, .T. ) ;
#6027=EDGE_LOOP ( 'NONE', ( #16776, #12729, #13319, #16243, #5416 ) ) ;
#6032=EDGE_CURVE ( 'NONE', #3717, #14752, #4370, .T. ) ;
#6036=DIRECTION ( 'NONE',  ( 0.000000000000000000, -0.000000000000000000, 1.000000000000000000 ) ) ;
#6037=LINE ( 'NONE', #9840, #1339 ) ;
#6041=LINE ( 'NONE', #7410, #15436 ) ;
#6042=ADVANCED_FACE ( 'NONE', ( #16044 ), #5650, .F. ) ;
#6045=ADVANCED_FACE ( 'NONE', ( #5386 ), #15863, .F. ) ;
#6052=CARTESIAN_POINT ( 'NONE',  ( 39.99999999999999289, 8.000000000000000000, 26.00000000000000000 ) ) ;
#6061=CYLINDRICAL_SURFACE ( 'NONE', #3087, 7.999999999999996447 ) ;
#6077=CARTESIAN_POINT ( 'NONE',  ( 22.99999999999998224, 6.000000000000000000, -36.99999999999999289 ) ) ;
#6087=DIRECTION ( 'NONE',  ( -0.000000000000000000, 1.000000000000000000, -0.000000000000000000 ) ) ;
#6095=ADVANCED_FACE ( 'NONE', ( #5296, #12185 ), #10897, .F. ) ;
#6111=LINE ( 'NONE', #12365, #14606 ) ;
#6121=DIRECTION ( 'NONE',  ( 0.000000000000000000, 0.000000000000000000, -1.000000000000000000 ) ) ;
#6124=CARTESIAN_POINT ( 'NONE',  ( 18.99999999999998224, 8.000000000000000000, -39.99999999999999289 ) ) ;
#6139=EDGE_CURVE ( 'NONE', #8527, #10488, #1615, .T. ) ;
#6145=VERTEX_POINT ( 'NONE', #4686 ) ;
#6152=DIRECTION ( 'NONE',  ( -0.000000000000000000, -1.000000000000000000, -0.000000000000000000 ) ) ;
#6157=CARTESIAN_POINT ( 'NONE',  ( 31.00000000000001421, 10.00000000000000000, 25.99999999999999645 ) ) ;
#6164=DIRECTION ( 'NONE',  ( 0.000000000000000000, 0.000000000000000000, -1.000000000000000000 ) ) ;
#6166=CARTESIAN_POINT ( 'NONE',  ( -31.00000000000001776, 10.00000000000000000, 31.00000000000000000 ) ) ;
#6167=VERTEX_POINT ( 'NONE', #9944 ) ;
#6170=CARTESIAN_POINT ( 'NONE',  ( -31.00000000000002132, 10.00000000000000000, -31.00000000000000000 ) ) ;
#6180=AXIS2_PLACEMENT_3D ( 'NONE', #9015, #10303, #12794 ) ;
#6188=VERTEX_POINT ( 'NONE', #12270 ) ;
#6199=LINE ( 'NONE', #5165, #5593 ) ;
#6201=EDGE_CURVE ( 'NONE', #9177, #6935, #3249, .T. ) ;
#6240=DIRECTION ( 'NONE',  ( 0.000000000000000000, 1.000000000000000000, 0.000000000000000000 ) ) ;
#6244=ORIENTED_EDGE ( 'NONE', *, *, #3634, .T. ) ;
#6248=ORIENTED_EDGE ( 'NONE', *, *, #6032, .T. ) ;
#6259=ORIENTED_EDGE ( 'NONE', *, *, #998, .T. ) ;
#6277=EDGE_CURVE ( 'NONE', #3043, #12295, #1947, .T. ) ;
#6283=VERTEX_POINT ( 'NONE', #4447 ) ;
#6286=ORIENTED_EDGE ( 'NONE', *, *, #8046, .T. ) ;
#6290=ORIENTED_EDGE ( 'NONE', *, *, #4267, .T. ) ;
#6309=VECTOR ( 'NONE', #1269, 1000.000000000000000 ) ;
#6312=EDGE_CURVE ( 'NONE', #5074, #3738, #11698, .T. ) ;
#6320=DIRECTION ( 'NONE',  ( 1.000000000000000000, 0.000000000000000000, -0.000000000000000000 ) ) ;
#6339=PLANE ( 'NONE',  #12360 ) ;
#6342=EDGE_CURVE ( 'NONE', #2707, #8178, #4145, .T. ) ;
#6355=VERTEX_POINT ( 'NONE', #11393 ) ;
#6380=DIRECTION ( 'NONE',  ( -0.000000000000000000, 0.000000000000000000, -1.000000000000000000 ) ) ;
#6411=DIRECTION ( 'NONE',  ( 0.000000000000000000, 0.000000000000000000, 1.000000000000000000 ) ) ;
#6424=CARTESIAN_POINT ( 'NONE',  ( 21.99999999999998224, 6.000000000000000000, -35.99999999999999289 ) ) ;
#6429=EDGE_CURVE ( 'NONE', #10488, #6355, #8363, .T. ) ;
#6436=EDGE_CURVE ( 'NONE', #5130, #10548, #6973, .T. ) ;
#6438=EDGE_CURVE ( 'NONE', #7594, #9955, #16085, .T. ) ;
#6439=EDGE_CURVE ( 'NONE', #4506, #6188, #16166, .T. ) ;
#6447=CARTESIAN_POINT ( 'NONE',  ( 39.99999999999999289, 8.000000000000000000, 18.99999999999999645 ) ) ;
#6465=SURFACE_STYLE_FILL_AREA ( #3662 ) ;
#6466=DIRECTION ( 'NONE',  ( -0.000000000000000000, -1.000000000000000000, 0.000000000000000000 ) ) ;
#6478=CARTESIAN_POINT ( 'NONE',  ( 21.99999999999998224, 10.00000000000000000, -32.99999999999999289 ) ) ;
#6491=ORIENTED_EDGE ( 'NONE', *, *, #2149, .F. ) ;
#6495=CARTESIAN_POINT ( 'NONE',  ( -36.00000000000000711, 10.00000000000000000, -18.00000000000000355 ) ) ;
#6502=VECTOR ( 'NONE', #13980, 1000.000000000000000 ) ;
#6509=CARTESIAN_POINT ( 'NONE',  ( -26.00000000000002132, 0.000000000000000000, 40.00000000000000711 ) ) ;
#6525=EDGE_LOOP ( 'NONE', ( #10883, #1036, #14709, #8103 ) ) ;
#6531=EDGE_LOOP ( 'NONE', ( #10830, #9968, #7733, #16713, #887 ) ) ;
#6545=ORIENTED_EDGE ( 'NONE', *, *, #10576, .F. ) ;
#6549=CARTESIAN_POINT ( 'NONE',  ( 22.99999999999998224, 6.000000000000000000, -31.99999999999998579 ) ) ;
#6553=PRODUCT_DEFINITION_SHAPE ( 'NONE', 'NONE',  #14937 ) ;
#6555=EDGE_CURVE ( 'NONE', #777, #11379, #15048, .T. ) ;
#6570=CARTESIAN_POINT ( 'NONE',  ( -33.00000000000000000, 8.000000000000000000, -22.00000000000000355 ) ) ;
#6571=DIRECTION ( 'NONE',  ( -1.156482317317881191E-15, 0.000000000000000000, -1.000000000000000000 ) ) ;
#6572=AXIS2_PLACEMENT_3D ( 'NONE', #6627, #11888, #131 ) ;
#6574=AXIS2_PLACEMENT_3D ( 'NONE', #7407, #7488, #1062 ) ;
#6589=CARTESIAN_POINT ( 'NONE',  ( -23.00000000000002487, 10.00000000000000000, -31.00000000000003553 ) ) ;
#6596=DIRECTION ( 'NONE',  ( -1.000000000000000000, -0.000000000000000000, -0.000000000000000000 ) ) ;
#6616=LINE ( 'NONE', #6447, #8600 ) ;
#6627=CARTESIAN_POINT ( 'NONE',  ( -23.00000000000002487, 10.00000000000000000, -31.00000000000003553 ) ) ;
#6629=CARTESIAN_POINT ( 'NONE',  ( 25.99999999999998224, 10.00000000000000000, -31.00000000000003197 ) ) ;
#6633=ORIENTED_EDGE ( 'NONE', *, *, #3109, .T. ) ;
#6636=DIRECTION ( 'NONE',  ( 0.000000000000000000, 0.000000000000000000, -1.000000000000000000 ) ) ;
#6641=CIRCLE ( 'NONE', #12147, 5.000000000000000888 ) ;
#6645=DIRECTION ( 'NONE',  ( -0.000000000000000000, 1.000000000000000000, -0.000000000000000000 ) ) ;
#6652=ORIENTED_EDGE ( 'NONE', *, *, #11590, .T. ) ;
#6656=VECTOR ( 'NONE', #12016, 1000.000000000000000 ) ;
#6657=AXIS2_PLACEMENT_3D ( 'NONE', #6170, #16260, #12621 ) ;
#6666=FACE_OUTER_BOUND ( 'NONE', #16209, .T. ) ;
#6668=VERTEX_POINT ( 'NONE', #12558 ) ;
#6676=LINE ( 'NONE', #168, #4019 ) ;
#6679=DIRECTION ( 'NONE',  ( -0.000000000000000000, -1.000000000000000000, 0.000000000000000000 ) ) ;
#6682=ORIENTED_EDGE ( 'NONE', *, *, #9472, .T. ) ;
#6686=EDGE_CURVE ( 'NONE', #15220, #7960, #965, .T. ) ;
#6707=ORIENTED_EDGE ( 'NONE', *, *, #14571, .F. ) ;
#6712=DIRECTION ( 'NONE',  ( 0.000000000000000000, 1.000000000000000000, 0.000000000000000000 ) ) ;
#6714=ORIENTED_EDGE ( 'NONE', *, *, #1654, .F. ) ;
#6715=VECTOR ( 'NONE', #5102, 1000.000000000000000 ) ;
#6718=EDGE_LOOP ( 'NONE', ( #11520, #127, #5375, #12417, #3195, #8306, #16167, #13858, #9016, #10153, #6823, #1263, #7091, #11266, #15363, #5086 ) ) ;
#6727=VECTOR ( 'NONE', #5258, 1000.000000000000000 ) ;
#6728=ORIENTED_EDGE ( 'NONE', *, *, #16865, .T. ) ;
#6739=AXIS2_PLACEMENT_3D ( 'NONE', #249, #10632, #16129 ) ;
#6753=EDGE_CURVE ( 'NONE', #2354, #6283, #15719, .T. ) ;
#6759=ADVANCED_FACE ( 'NONE', ( #15473 ), #10484, .F. ) ;
#6765=AXIS2_PLACEMENT_3D ( 'NONE', #16705, #1007, #14375 ) ;
#6783=EDGE_CURVE ( 'NONE', #11935, #5229, #1570, .T. ) ;
#6785=CARTESIAN_POINT ( 'NONE',  ( 18.99999999999998224, 10.00000000000000000, -39.99999999999999289 ) ) ;
#6789=ORIENTED_EDGE ( 'NONE', *, *, #8753, .F. ) ;
#6794=ORIENTED_EDGE ( 'NONE', *, *, #7672, .T. ) ;
#6803=CARTESIAN_POINT ( 'NONE',  ( -40.00000000000000711, 8.000000000000000000, -19.00000000000000355 ) ) ;
#6806=DIRECTION ( 'NONE',  ( -0.000000000000000000, -1.000000000000000000, 0.000000000000000000 ) ) ;
#6820=LINE ( 'NONE', #5371, #16508 ) ;
#6823=ORIENTED_EDGE ( 'NONE', *, *, #11216, .F. ) ;
#6834=CARTESIAN_POINT ( 'NONE',  ( -18.00000000000001421, 10.00000000000000000, 37.00000000000000711 ) ) ;
#6836=CARTESIAN_POINT ( 'NONE',  ( -23.00000000000002487, 10.00000000000000000, -31.00000000000003553 ) ) ;
#6850=VECTOR ( 'NONE', #13028, 1000.000000000000000 ) ;
#6856=ORIENTED_EDGE ( 'NONE', *, *, #3304, .T. ) ;
#6863=ORIENTED_EDGE ( 'NONE', *, *, #1546, .T. ) ;
#6865=CARTESIAN_POINT ( 'NONE',  ( 22.99999999999998224, 0.000000000000000000, -31.00000000000003197 ) ) ;
#6886=CIRCLE ( 'NONE', #5223, 5.000000000000000888 ) ;
#6901=DIRECTION ( 'NONE',  ( -1.000000000000000000, 0.000000000000000000, -1.734723475976807094E-15 ) ) ;
#6905=VECTOR ( 'NONE', #10717, 1000.000000000000000 ) ;
#6912=ORIENTED_EDGE ( 'NONE', *, *, #12545, .T. ) ;
#6932=DIRECTION ( 'NONE',  ( 0.000000000000000000, 1.000000000000000000, -0.000000000000000000 ) ) ;
#6935=VERTEX_POINT ( 'NONE', #1640 ) ;
#6949=CARTESIAN_POINT ( 'NONE',  ( -26.00000000000002132, 10.00000000000000000, -39.99999999999999289 ) ) ;
#6958=EDGE_CURVE ( 'NONE', #2938, #14585, #5584, .T. ) ;
#6973=LINE ( 'NONE', #9566, #5392 ) ;
#6977=ORIENTED_EDGE ( 'NONE', *, *, #11141, .F. ) ;
#7025=DIRECTION ( 'NONE',  ( 0.000000000000000000, 0.000000000000000000, 1.000000000000000000 ) ) ;
#7061=CARTESIAN_POINT ( 'NONE',  ( -19.00000000000001776, 8.000000000000000000, 36.00000000000000711 ) ) ;
#7062=EDGE_CURVE ( 'NONE', #1606, #14752, #859, .T. ) ;
#7064=ORIENTED_EDGE ( 'NONE', *, *, #7394, .T. ) ;
#7069=DIRECTION ( 'NONE',  ( 1.000000000000000000, 0.000000000000000000, 0.000000000000000000 ) ) ;
#7071=DIRECTION ( 'NONE',  ( 1.734723475976807094E-15, 0.000000000000000000, -1.000000000000000000 ) ) ;
#7079=LINE ( 'NONE', #11130, #15087 ) ;
#7089=EDGE_CURVE ( 'NONE', #15120, #15290, #3467, .T. ) ;
#7091=ORIENTED_EDGE ( 'NONE', *, *, #1916, .F. ) ;
#7100=CARTESIAN_POINT ( 'NONE',  ( 21.99999999999998224, 6.000000000000000000, -35.99999999999999289 ) ) ;
#7114=DIRECTION ( 'NONE',  ( 0.000000000000000000, 0.000000000000000000, -1.000000000000000000 ) ) ;
#7122=CIRCLE ( 'NONE', #13188, 3.000000000000002665 ) ;
#7126=LINE ( 'NONE', #12383, #1145 ) ;
#7129=ORIENTED_EDGE ( 'NONE', *, *, #16630, .F. ) ;
#7141=ORIENTED_EDGE ( 'NONE', *, *, #7826, .T. ) ;
#7147=DIRECTION ( 'NONE',  ( -8.673617379884027583E-16, 0.000000000000000000, 1.000000000000000000 ) ) ;
#7154=AXIS2_PLACEMENT_3D ( 'NONE', #7539, #6679, #10557 ) ;
#7160=EDGE_CURVE ( 'NONE', #15552, #16255, #14170, .T. ) ;
#7182=ADVANCED_FACE ( 'NONE', ( #12870 ), #11667, .T. ) ;
#7189=VERTEX_POINT ( 'NONE', #6495 ) ;
#7192=ORIENTED_EDGE ( 'NONE', *, *, #8848, .F. ) ;
#7198=ORIENTED_EDGE ( 'NONE', *, *, #4882, .F. ) ;
#7199=DIRECTION ( 'NONE',  ( 1.000000000000000000, 0.000000000000000000, 0.000000000000000000 ) ) ;
#7253=VECTOR ( 'NONE', #9613, 1000.000000000000000 ) ;
#7263=ORIENTED_EDGE ( 'NONE', *, *, #5204, .F. ) ;
#7268=DIRECTION ( 'NONE',  ( 0.000000000000000000, 1.000000000000000000, 0.000000000000000000 ) ) ;
#7269=FACE_OUTER_BOUND ( 'NONE', #6525, .T. ) ;
#7273=LINE ( 'NONE', #11316, #7930 ) ;
#7278=DIRECTION ( 'NONE',  ( -0.000000000000000000, 0.000000000000000000, 1.000000000000000000 ) ) ;
#7290=VECTOR ( 'NONE', #4804, 1000.000000000000000 ) ;
#7314=ORIENTED_EDGE ( 'NONE', *, *, #7160, .F. ) ;
#7325=FACE_OUTER_BOUND ( 'NONE', #5516, .T. ) ;
#7361=LINE ( 'NONE', #3265, #13887 ) ;
#7367=ADVANCED_FACE ( 'NONE', ( #16133 ), #16049, .F. ) ;
#7369=DIRECTION ( 'NONE',  ( 0.000000000000000000, 0.000000000000000000, 1.000000000000000000 ) ) ;
#7379=VERTEX_POINT ( 'NONE', #9529 ) ;
#7385=VERTEX_POINT ( 'NONE', #9440 ) ;
#7394=EDGE_CURVE ( 'NONE', #16255, #12090, #6676, .T. ) ;
#7404=DIRECTION ( 'NONE',  ( -0.000000000000000000, -1.000000000000000000, -0.000000000000000000 ) ) ;
#7407=CARTESIAN_POINT ( 'NONE',  ( 18.99999999999998224, 8.000000000000000000, -39.99999999999999289 ) ) ;
#7409=DIRECTION ( 'NONE',  ( -0.000000000000000000, -1.000000000000000000, -0.000000000000000000 ) ) ;
#7410=CARTESIAN_POINT ( 'NONE',  ( -32.00000000000000711, 6.000000000000000000, -22.00000000000000355 ) ) ;
#7420=AXIS2_PLACEMENT_3D ( 'NONE', #7759, #13021, #9154 ) ;
#7428=CARTESIAN_POINT ( 'NONE',  ( 35.99999999999999289, 10.00000000000000000, 18.99999999999999289 ) ) ;
#7433=PLANE ( 'NONE',  #16855 ) ;
#7434=CARTESIAN_POINT ( 'NONE',  ( 31.00000000000001421, 0.000000000000000000, 22.99999999999999645 ) ) ;
#7437=DIRECTION ( 'NONE',  ( -1.000000000000000000, 0.000000000000000000, -0.000000000000000000 ) ) ;
#7438=ORIENTED_EDGE ( 'NONE', *, *, #5727, .T. ) ;
#7451=CARTESIAN_POINT ( 'NONE',  ( 31.99999999999998579, 6.000000000000000000, 25.99999999999999645 ) ) ;
#7475=AXIS2_PLACEMENT_3D ( 'NONE', #3620, #8701, #13759 ) ;
#7483=CARTESIAN_POINT ( 'NONE',  ( -22.00000000000001776, 6.000000000000000000, 32.00000000000000711 ) ) ;
#7488=DIRECTION ( 'NONE',  ( -1.000000000000000000, 0.000000000000000000, 0.000000000000000000 ) ) ;
#7492=ORIENTED_EDGE ( 'NONE', *, *, #14479, .F. ) ;
#7495=ADVANCED_BREP_SHAPE_REPRESENTATION ( '', ( #14111, #1488 ), #13563 ) ;
#7510=CARTESIAN_POINT ( 'NONE',  ( 21.99999999999998224, 10.00000000000000000, -35.99999999999999289 ) ) ;
#7522=FACE_OUTER_BOUND ( 'NONE', #3679, .T. ) ;
#7533=PLANE ( 'NONE',  #3204 ) ;
#7538=ORIENTED_EDGE ( 'NONE', *, *, #6429, .T. ) ;
#7539=CARTESIAN_POINT ( 'NONE',  ( 30.99999999999997513, 10.00000000000000000, 30.99999999999999645 ) ) ;
#7543=LINE ( 'NONE', #3783, #5047 ) ;
#7552=DIRECTION ( 'NONE',  ( 0.000000000000000000, 1.000000000000000000, 0.000000000000000000 ) ) ;
#7559=ORIENTED_EDGE ( 'NONE', *, *, #13723, .T. ) ;
#7566=ORIENTED_EDGE ( 'NONE', *, *, #11694, .F. ) ;
#7569=CARTESIAN_POINT ( 'NONE',  ( 31.99999999999998579, 6.000000000000000000, 22.99999999999999645 ) ) ;
#7587=CARTESIAN_POINT ( 'NONE',  ( 25.99999999999998224, 0.000000000000000000, -31.00000000000003197 ) ) ;
#7594=VERTEX_POINT ( 'NONE', #5187 ) ;
#7600=PLANE ( 'NONE',  #9678 ) ;
#7616=DIRECTION ( 'NONE',  ( 0.000000000000000000, 1.000000000000000000, 0.000000000000000000 ) ) ;
#7619=DIRECTION ( 'NONE',  ( -0.000000000000000000, -0.000000000000000000, 1.000000000000000000 ) ) ;
#7632=EDGE_LOOP ( 'NONE', ( #16848, #3995, #4220, #1184, #12968 ) ) ;
#7643=ORIENTED_EDGE ( 'NONE', *, *, #463, .T. ) ;
#7657=EDGE_LOOP ( 'NONE', ( #6248, #10704, #8280, #8364 ) ) ;
#7663=LINE ( 'NONE', #6629, #6727 ) ;
#7665=VECTOR ( 'NONE', #7619, 1000.000000000000000 ) ;
#7669=DIRECTION ( 'NONE',  ( 0.000000000000000000, 0.000000000000000000, 1.000000000000000000 ) ) ;
#7672=EDGE_CURVE ( 'NONE', #9768, #5130, #9507, .T. ) ;
#7682=DIRECTION ( 'NONE',  ( 0.000000000000000000, 1.000000000000000000, 0.000000000000000000 ) ) ;
#7695=CARTESIAN_POINT ( 'NONE',  ( -22.00000000000001776, 10.00000000000000000, 36.00000000000000711 ) ) ;
#7708=VECTOR ( 'NONE', #591, 1000.000000000000000 ) ;
#7724=EDGE_CURVE ( 'NONE', #295, #4908, #10528, .T. ) ;
#7733=ORIENTED_EDGE ( 'NONE', *, *, #3119, .F. ) ;
#7738=ORIENTED_EDGE ( 'NONE', *, *, #3185, .F. ) ;
#7741=VECTOR ( 'NONE', #216, 1000.000000000000000 ) ;
#7749=ORIENTED_EDGE ( 'NONE', *, *, #12600, .F. ) ;
#7759=CARTESIAN_POINT ( 'NONE',  ( -22.00000000000001776, 8.000000000000000000, 36.00000000000000711 ) ) ;
#7767=DIRECTION ( 'NONE',  ( -1.000000000000000000, 0.000000000000000000, -8.673617379884027583E-16 ) ) ;
#7776=VECTOR ( 'NONE', #5886, 1000.000000000000000 ) ;
#7779=LINE ( 'NONE', #13040, #6309 ) ;
#7804=EDGE_CURVE ( 'NONE', #3015, #15220, #16365, .T. ) ;
#7805=ORIENTED_EDGE ( 'NONE', *, *, #5727, .F. ) ;
#7823=EDGE_CURVE ( 'NONE', #11352, #2454, #3310, .T. ) ;
#7826=EDGE_CURVE ( 'NONE', #5640, #10374, #491, .T. ) ;
#7849=VECTOR ( 'NONE', #6645, 1000.000000000000000 ) ;
#7857=DIRECTION ( 'NONE',  ( 0.000000000000000000, 0.000000000000000000, -1.000000000000000000 ) ) ;
#7868=LINE ( 'NONE', #1436, #7967 ) ;
#7891=DIRECTION ( 'NONE',  ( -0.000000000000000000, 1.000000000000000000, -0.000000000000000000 ) ) ;
#7898=ORIENTED_EDGE ( 'NONE', *, *, #65, .F. ) ;
#7901=ORIENTED_EDGE ( 'NONE', *, *, #7724, .F. ) ;
#7912=ORIENTED_EDGE ( 'NONE', *, *, #5874, .T. ) ;
#7930=VECTOR ( 'NONE', #14945, 1000.000000000000000 ) ;
#7934=DIRECTION ( 'NONE',  ( -1.000000000000000000, -0.000000000000000000, 3.854941057726258312E-16 ) ) ;
#7936=CARTESIAN_POINT ( 'NONE',  ( 25.99999999999998224, 6.000000000000000000, -31.99999999999998579 ) ) ;
#7938=FACE_OUTER_BOUND ( 'NONE', #5844, .T. ) ;
#7945=CARTESIAN_POINT ( 'NONE',  ( -23.00000000000002132, 6.000000000000000000, 37.00000000000000711 ) ) ;
#7946=CARTESIAN_POINT ( 'NONE',  ( 21.99999999999998224, 8.000000000000000000, -32.99999999999999289 ) ) ;
#7957=DIRECTION ( 'NONE',  ( 0.000000000000000000, 0.000000000000000000, -1.000000000000000000 ) ) ;
#7960=VERTEX_POINT ( 'NONE', #6124 ) ;
#7967=VECTOR ( 'NONE', #243, 1000.000000000000000 ) ;
#7968=CARTESIAN_POINT ( 'NONE',  ( 25.99999999999998224, 8.000000000000000000, -32.99999999999999289 ) ) ;
#7969=FACE_OUTER_BOUND ( 'NONE', #3778, .T. ) ;
#7971=DIRECTION ( 'NONE',  ( 3.854941057726254860E-16, 0.000000000000000000, -1.000000000000000000 ) ) ;
#7986=ORIENTED_EDGE ( 'NONE', *, *, #6139, .F. ) ;
#7997=EDGE_CURVE ( 'NONE', #15120, #16566, #2264, .T. ) ;
#8020=EDGE_CURVE ( 'NONE', #9955, #4912, #16938, .T. ) ;
#8021=LINE ( 'NONE', #397, #13280 ) ;
#8026=AXIS2_PLACEMENT_3D ( 'NONE', #3398, #8642, #13873 ) ;
#8027=AXIS2_PLACEMENT_3D ( 'NONE', #1270, #5199, #15608 ) ;
#8042=DIRECTION ( 'NONE',  ( 0.000000000000000000, 0.000000000000000000, -1.000000000000000000 ) ) ;
#8046=EDGE_CURVE ( 'NONE', #3745, #2354, #12834, .T. ) ;
#8047=ORIENTED_EDGE ( 'NONE', *, *, #714, .T. ) ;
#8053=ORIENTED_EDGE ( 'NONE', *, *, #65, .T. ) ;
#8080=VECTOR ( 'NONE', #7891, 1000.000000000000000 ) ;
#8103=ORIENTED_EDGE ( 'NONE', *, *, #6438, .T. ) ;
#8112=ORIENTED_EDGE ( 'NONE', *, *, #15649, .T. ) ;
#8123=AXIS2_PLACEMENT_3D ( 'NONE', #941, #16226, #4466 ) ;
#8129=LINE ( 'NONE', #7946, #14536 ) ;
#8133=CARTESIAN_POINT ( 'NONE',  ( 22.99999999999997513, 0.000000000000000000, 31.00000000000005684 ) ) ;
#8139=ORIENTED_EDGE ( 'NONE', *, *, #8558, .T. ) ;
#8141=DIRECTION ( 'NONE',  ( 1.000000000000000000, 0.000000000000000000, 8.673617379884027583E-16 ) ) ;
#8155=EDGE_CURVE ( 'NONE', #10824, #8801, #2954, .T. ) ;
#8162=CARTESIAN_POINT ( 'NONE',  ( -40.00000000000000711, 8.000000000000000000, -26.00000000000000000 ) ) ;
#8164=FACE_OUTER_BOUND ( 'NONE', #3342, .T. ) ;
#8170=VERTEX_POINT ( 'NONE', #13177 ) ;
#8175=ORIENTED_EDGE ( 'NONE', *, *, #6958, .T. ) ;
#8178=VERTEX_POINT ( 'NONE', #1497 ) ;
#8203=LINE ( 'NONE', #4664, #4129 ) ;
#8205=DIRECTION ( 'NONE',  ( -1.000000000000000000, -0.000000000000000000, -0.000000000000000000 ) ) ;
#8220=AXIS2_PLACEMENT_3D ( 'NONE', #3678, #7682, #10534 ) ;
#8229=ORIENTED_EDGE ( 'NONE', *, *, #6139, .T. ) ;
#8232=VECTOR ( 'NONE', #16911, 1000.000000000000000 ) ;
#8260=EDGE_LOOP ( 'NONE', ( #6728, #12642, #16676, #11953 ) ) ;
#8280=ORIENTED_EDGE ( 'NONE', *, *, #9489, .F. ) ;
#8289=CARTESIAN_POINT ( 'NONE',  ( -23.00000000000002132, 0.000000000000000000, 37.00000000000000711 ) ) ;
#8292=FACE_OUTER_BOUND ( 'NONE', #8260, .T. ) ;
#8306=ORIENTED_EDGE ( 'NONE', *, *, #11710, .F. ) ;
#8307=DIRECTION ( 'NONE',  ( 0.000000000000000000, 0.000000000000000000, -1.000000000000000000 ) ) ;
#8318=AXIS2_PLACEMENT_3D ( 'NONE', #4857, #4608, #4772 ) ;
#8326=LINE ( 'NONE', #5573, #16522 ) ;
#8348=VERTEX_POINT ( 'NONE', #10135 ) ;
#8352=EDGE_CURVE ( 'NONE', #10374, #1948, #8369, .T. ) ;
#8363=LINE ( 'NONE', #13608, #13359 ) ;
#8364=ORIENTED_EDGE ( 'NONE', *, *, #16233, .T. ) ;
#8369=LINE ( 'NONE', #7451, #5400 ) ;
#8377=CYLINDRICAL_SURFACE ( 'NONE', #729, 2.999999999999995559 ) ;
#8391=CARTESIAN_POINT ( 'NONE',  ( 31.00000000000003553, 10.00000000000000000, -22.99999999999999645 ) ) ;
#8392=CARTESIAN_POINT ( 'NONE',  ( 30.99999999999997868, 0.000000000000000000, -30.99999999999999645 ) ) ;
#8409=EDGE_CURVE ( 'NONE', #11373, #4234, #3696, .T. ) ;
#8423=VECTOR ( 'NONE', #10011, 1000.000000000000000 ) ;
#8437=ORIENTED_EDGE ( 'NONE', *, *, #7672, .F. ) ;
#8448=EDGE_CURVE ( 'NONE', #10067, #11352, #2565, .T. ) ;
#8451=ORIENTED_EDGE ( 'NONE', *, *, #8409, .T. ) ;
#8461=FACE_OUTER_BOUND ( 'NONE', #7657, .T. ) ;
#8483=EDGE_CURVE ( 'NONE', #594, #4006, #255, .T. ) ;
#8489=CARTESIAN_POINT ( 'NONE',  ( 30.99999999999997868, 10.00000000000000000, -30.99999999999999645 ) ) ;
#8498=AXIS2_PLACEMENT_3D ( 'NONE', #13575, #9619, #7025 ) ;
#8499=ORIENTED_EDGE ( 'NONE', *, *, #1916, .T. ) ;
#8502=ORIENTED_EDGE ( 'NONE', *, *, #9518, .F. ) ;
#8527=VERTEX_POINT ( 'NONE', #13403 ) ;
#8545=PLANE ( 'NONE',  #2259 ) ;
#8556=ORIENTED_EDGE ( 'NONE', *, *, #16642, .F. ) ;
#8558=EDGE_CURVE ( 'NONE', #1379, #14282, #3505, .T. ) ;
#8559=EDGE_CURVE ( 'NONE', #14542, #221, #11401, .T. ) ;
#8569=FACE_OUTER_BOUND ( 'NONE', #5091, .T. ) ;
#8574=CARTESIAN_POINT ( 'NONE',  ( -37.00000000000000711, 10.00000000000000000, -23.00000000000000000 ) ) ;
#8582=EDGE_CURVE ( 'NONE', #7385, #8170, #16388, .T. ) ;
#8584=ADVANCED_FACE ( 'NONE', ( #7269 ), #4693, .T. ) ;
#8593=AXIS2_PLACEMENT_3D ( 'NONE', #14243, #2461, #16888 ) ;
#8600=VECTOR ( 'NONE', #1490, 1000.000000000000000 ) ;
#8614=ORIENTED_EDGE ( 'NONE', *, *, #7089, .F. ) ;
#8637=CARTESIAN_POINT ( 'NONE',  ( -37.00000000000000711, 10.00000000000000000, -18.00000000000000355 ) ) ;
#8640=EDGE_LOOP ( 'NONE', ( #15654, #5676, #839, #3983 ) ) ;
#8642=DIRECTION ( 'NONE',  ( 1.000000000000000000, -0.000000000000000000, 0.000000000000000000 ) ) ;
#8643=EDGE_CURVE ( 'NONE', #4006, #6188, #2205, .T. ) ;
#8651=PLANE ( 'NONE',  #8318 ) ;
#8662=EDGE_CURVE ( 'NONE', #11763, #5640, #3256, .T. ) ;
#8677=CARTESIAN_POINT ( 'NONE',  ( -40.00000000000000711, 10.00000000000000000, 26.00000000000000000 ) ) ;
#8689=ORIENTED_EDGE ( 'NONE', *, *, #6277, .T. ) ;
#8693=DIRECTION ( 'NONE',  ( 0.000000000000000000, 0.000000000000000000, 1.000000000000000000 ) ) ;
#8699=DIRECTION ( 'NONE',  ( -0.000000000000000000, 1.000000000000000000, -0.000000000000000000 ) ) ;
#8701=DIRECTION ( 'NONE',  ( -1.000000000000000000, 0.000000000000000000, 1.156482317317881191E-15 ) ) ;
#8703=ORIENTED_EDGE ( 'NONE', *, *, #231, .T. ) ;
#8704=EDGE_CURVE ( 'NONE', #529, #9900, #14311, .T. ) ;
#8716=LINE ( 'NONE', #16431, #13206 ) ;
#8717=CARTESIAN_POINT ( 'NONE',  ( -31.00000000000001776, 0.000000000000000000, 31.00000000000000000 ) ) ;
#8720=CARTESIAN_POINT ( 'NONE',  ( 30.99999999999997868, 10.00000000000000000, -30.99999999999999645 ) ) ;
#8723=CARTESIAN_POINT ( 'NONE',  ( 31.00000000000003553, 10.00000000000000000, -23.00000000000000000 ) ) ;
#8730=VECTOR ( 'NONE', #12439, 1000.000000000000000 ) ;
#8737=ORIENTED_EDGE ( 'NONE', *, *, #16845, .T. ) ;
#8748=LINE ( 'NONE', #932, #708 ) ;
#8751=FACE_OUTER_BOUND ( 'NONE', #10399, .T. ) ;
#8752=EDGE_CURVE ( 'NONE', #8170, #1977, #2452, .T. ) ;
#8753=EDGE_CURVE ( 'NONE', #1606, #16501, #15358, .T. ) ;
#8757=ORIENTED_EDGE ( 'NONE', *, *, #16269, .F. ) ;
#8773=ORIENTED_EDGE ( 'NONE', *, *, #3913, .F. ) ;
#8801=VERTEX_POINT ( 'NONE', #11818 ) ;
#8803=LINE ( 'NONE', #11457, #14605 ) ;
#8810=VERTEX_POINT ( 'NONE', #61 ) ;
#8813=AXIS2_PLACEMENT_3D ( 'NONE', #14393, #7669, #10280 ) ;
#8816=LINE ( 'NONE', #3413, #14946 ) ;
#8819=CARTESIAN_POINT ( 'NONE',  ( 35.99999999999999289, 8.000000000000000000, 21.99999999999999645 ) ) ;
#8822=CARTESIAN_POINT ( 'NONE',  ( 35.99999999999999289, 8.000000000000000000, 21.99999999999999645 ) ) ;
#8827=CARTESIAN_POINT ( 'NONE',  ( 32.99999999999998579, 8.000000000000000000, 25.99999999999999645 ) ) ;
#8832=CARTESIAN_POINT ( 'NONE',  ( 39.99999999999999289, 10.00000000000000000, -26.00000000000000000 ) ) ;
#8833=ORIENTED_EDGE ( 'NONE', *, *, #10576, .T. ) ;
#8843=CARTESIAN_POINT ( 'NONE',  ( 35.99999999999999289, 10.00000000000000000, 21.99999999999999645 ) ) ;
#8848=EDGE_CURVE ( 'NONE', #6167, #2142, #153, .T. ) ;
#8852=CARTESIAN_POINT ( 'NONE',  ( -33.00000000000000000, 8.000000000000000000, -22.00000000000000355 ) ) ;
#8863=CIRCLE ( 'NONE', #12428, 8.000000000000000000 ) ;
#8867=ORIENTED_EDGE ( 'NONE', *, *, #3092, .T. ) ;
#8874=ORIENTED_EDGE ( 'NONE', *, *, #5499, .F. ) ;
#8879=LINE ( 'NONE', #14369, #5300 ) ;
#8883=DIRECTION ( 'NONE',  ( 1.000000000000000000, -0.000000000000000000, 0.000000000000000000 ) ) ;
#8885=VECTOR ( 'NONE', #5624, 1000.000000000000000 ) ;
#8888=CYLINDRICAL_SURFACE ( 'NONE', #9135, 8.000000000000000000 ) ;
#8890=ORIENTED_EDGE ( 'NONE', *, *, #5, .F. ) ;
#8895=EDGE_CURVE ( 'NONE', #2103, #16003, #14668, .T. ) ;
#8896=EDGE_CURVE ( 'NONE', #7385, #3015, #8129, .T. ) ;
#8912=LINE ( 'NONE', #14150, #2201 ) ;
#8913=AXIS2_PLACEMENT_3D ( 'NONE', #16788, #5269, #52 ) ;
#8921=CARTESIAN_POINT ( 'NONE',  ( -37.00000000000000711, 0.000000000000000000, -23.00000000000000000 ) ) ;
#8924=VERTEX_POINT ( 'NONE', #12082 ) ;
#8928=CARTESIAN_POINT ( 'NONE',  ( -19.00000000000001776, 8.000000000000000000, 40.00000000000000711 ) ) ;
#8933=ORIENTED_EDGE ( 'NONE', *, *, #9489, .T. ) ;
#8934=CARTESIAN_POINT ( 'NONE',  ( -26.00000000000002132, 0.000000000000000000, -31.00000000000003553 ) ) ;
#8935=DIRECTION ( 'NONE',  ( -0.000000000000000000, 1.000000000000000000, -0.000000000000000000 ) ) ;
#8944=DIRECTION ( 'NONE',  ( 0.000000000000000000, 1.000000000000000000, 0.000000000000000000 ) ) ;
#8995=CARTESIAN_POINT ( 'NONE',  ( -37.00000000000000711, 10.00000000000000000, 23.00000000000000000 ) ) ;
#9008=EDGE_CURVE ( 'NONE', #2065, #1379, #11289, .T. ) ;
#9009=VECTOR ( 'NONE', #6596, 1000.000000000000000 ) ;
#9011=FACE_OUTER_BOUND ( 'NONE', #10915, .T. ) ;
#9015=CARTESIAN_POINT ( 'NONE',  ( 36.99999999999999289, 10.00000000000000000, 22.99999999999999645 ) ) ;
#9016=ORIENTED_EDGE ( 'NONE', *, *, #281, .F. ) ;
#9028=FACE_OUTER_BOUND ( 'NONE', #706, .T. ) ;
#9034=CARTESIAN_POINT ( 'NONE',  ( -32.00000000000000711, 10.00000000000000000, -22.00000000000000355 ) ) ;
#9035=ORIENTED_EDGE ( 'NONE', *, *, #9811, .T. ) ;
#9041=EDGE_LOOP ( 'NONE', ( #16922, #15392, #12673, #1371 ) ) ;
#9066=PLANE ( 'NONE',  #8913 ) ;
#9068=EDGE_CURVE ( 'NONE', #4162, #4234, #7079, .T. ) ;
#9069=FACE_OUTER_BOUND ( 'NONE', #432, .T. ) ;
#9082=DIRECTION ( 'NONE',  ( 1.000000000000000000, 0.000000000000000000, 0.000000000000000000 ) ) ;
#9085=DIRECTION ( 'NONE',  ( 1.000000000000000000, 0.000000000000000000, -0.000000000000000000 ) ) ;
#9092=VERTEX_POINT ( 'NONE', #11630 ) ;
#9107=ORIENTED_EDGE ( 'NONE', *, *, #13398, .F. ) ;
#9115=CARTESIAN_POINT ( 'NONE',  ( -23.00000000000002132, 0.000000000000000000, 37.00000000000000711 ) ) ;
#9131=DIRECTION ( 'NONE',  ( 0.000000000000000000, 1.000000000000000000, -0.000000000000000000 ) ) ;
#9135=AXIS2_PLACEMENT_3D ( 'NONE', #14131, #2346, #15742 ) ;
#9138=FACE_OUTER_BOUND ( 'NONE', #5821, .T. ) ;
#9139=VECTOR ( 'NONE', #5264, 1000.000000000000000 ) ;
#9154=DIRECTION ( 'NONE',  ( 0.000000000000000000, -0.000000000000000000, 1.000000000000000000 ) ) ;
#9168=ORIENTED_EDGE ( 'NONE', *, *, #10151, .F. ) ;
#9177=VERTEX_POINT ( 'NONE', #11718 ) ;
#9182=DIRECTION ( 'NONE',  ( 0.000000000000000000, 1.000000000000000000, 0.000000000000000000 ) ) ;
#9184=LINE ( 'NONE', #11573, #7665 ) ;
#9185=VECTOR ( 'NONE', #3361, 1000.000000000000000 ) ;
#9204=DIRECTION ( 'NONE',  ( 1.000000000000000000, 0.000000000000000000, 8.673617379884027583E-16 ) ) ;
#9205=ORIENTED_EDGE ( 'NONE', *, *, #4384, .F. ) ;
#9209=DIRECTION ( 'NONE',  ( 0.000000000000000000, 1.000000000000000000, 0.000000000000000000 ) ) ;
#9213=ORIENTED_EDGE ( 'NONE', *, *, #4192, .F. ) ;
#9224=LINE ( 'NONE', #10589, #12735 ) ;
#9227=DIRECTION ( 'NONE',  ( 0.000000000000000000, 0.000000000000000000, 1.000000000000000000 ) ) ;
#9234=VERTEX_POINT ( 'NONE', #6803 ) ;
#9242=DIRECTION ( 'NONE',  ( 0.000000000000000000, 0.000000000000000000, -1.000000000000000000 ) ) ;
#9246=VECTOR ( 'NONE', #15904, 1000.000000000000000 ) ;
#9253=CARTESIAN_POINT ( 'NONE',  ( 22.99999999999998224, 10.00000000000000000, -31.99999999999998579 ) ) ;
#9268=CARTESIAN_POINT ( 'NONE',  ( -36.00000000000000711, 10.00000000000000000, -22.00000000000000355 ) ) ;
#9273=CARTESIAN_POINT ( 'NONE',  ( -37.00000000000000711, 6.000000000000000000, -23.00000000000000000 ) ) ;
#9296=ADVANCED_FACE ( 'NONE', ( #13180 ), #1406, .T. ) ;
#9297=ORIENTED_EDGE ( 'NONE', *, *, #9008, .F. ) ;
#9301=CARTESIAN_POINT ( 'NONE',  ( -32.00000000000000711, 6.000000000000000000, -22.00000000000000355 ) ) ;
#9305=VERTEX_POINT ( 'NONE', #9312 ) ;
#9311=ORIENTED_EDGE ( 'NONE', *, *, #6011, .F. ) ;
#9312=CARTESIAN_POINT ( 'NONE',  ( 22.99999999999998224, 10.00000000000000000, 37.00000000000000711 ) ) ;
#9332=AXIS2_PLACEMENT_3D ( 'NONE', #12684, #16876, #923 ) ;
#9333=DIRECTION ( 'NONE',  ( 0.000000000000000000, 0.000000000000000000, -1.000000000000000000 ) ) ;
#9337=CARTESIAN_POINT ( 'NONE',  ( 36.99999999999999289, 0.000000000000000000, 22.99999999999999645 ) ) ;
#9345=ORIENTED_EDGE ( 'NONE', *, *, #14921, .F. ) ;
#9347=ADVANCED_FACE ( 'NONE', ( #9028 ), #6339, .T. ) ;
#9358=DIRECTION ( 'NONE',  ( -3.854941057726255847E-16, -0.000000000000000000, 1.000000000000000000 ) ) ;
#9363=DIRECTION ( 'NONE',  ( 3.854941057726254367E-16, 0.000000000000000000, 1.000000000000000000 ) ) ;
#9366=LINE ( 'NONE', #2839, #9009 ) ;
#9372=ORIENTED_EDGE ( 'NONE', *, *, #16956, .F. ) ;
#9385=DIRECTION ( 'NONE',  ( 0.000000000000000000, 1.000000000000000000, 0.000000000000000000 ) ) ;
#9387=CARTESIAN_POINT ( 'NONE',  ( -23.00000000000002132, 10.00000000000000000, 32.00000000000000000 ) ) ;
#9391=DIRECTION ( 'NONE',  ( 0.000000000000000000, 0.000000000000000000, 1.000000000000000000 ) ) ;
#9399=ORIENTED_EDGE ( 'NONE', *, *, #9488, .F. ) ;
#9413=EDGE_CURVE ( 'NONE', #8924, #6167, #4937, .T. ) ;
#9420=DIRECTION ( 'NONE',  ( 1.000000000000000000, -0.000000000000000000, 0.000000000000000000 ) ) ;
#9428=CARTESIAN_POINT ( 'NONE',  ( -40.00000000000000711, 10.00000000000000000, -26.00000000000000000 ) ) ;
#9429=PLANE ( 'NONE',  #913 ) ;
#9435=CARTESIAN_POINT ( 'NONE',  ( -36.00000000000000711, 6.000000000000000000, -22.00000000000000355 ) ) ;
#9439=VECTOR ( 'NONE', #7069, 1000.000000000000000 ) ;
#9440=CARTESIAN_POINT ( 'NONE',  ( 21.99999999999998224, 8.000000000000000000, -32.99999999999999289 ) ) ;
#9460=DIRECTION ( 'NONE',  ( -0.000000000000000000, -1.000000000000000000, 0.000000000000000000 ) ) ;
#9466=ORIENTED_EDGE ( 'NONE', *, *, #16845, .F. ) ;
#9472=EDGE_CURVE ( 'NONE', #5278, #3550, #837, .T. ) ;
#9488=EDGE_CURVE ( 'NONE', #6283, #5074, #11509, .T. ) ;
#9489=EDGE_CURVE ( 'NONE', #9234, #1606, #15715, .T. ) ;
#9496=ADVANCED_FACE ( 'NONE', ( #3709 ), #2404, .F. ) ;
#9497=ORIENTED_EDGE ( 'NONE', *, *, #16956, .T. ) ;
#9499=LINE ( 'NONE', #14738, #15655 ) ;
#9507=LINE ( 'NONE', #2885, #7849 ) ;
#9513=ORIENTED_EDGE ( 'NONE', *, *, #1107, .T. ) ;
#9515=EDGE_CURVE ( 'NONE', #16501, #16504, #10142, .T. ) ;
#9518=EDGE_CURVE ( 'NONE', #2662, #7189, #7868, .T. ) ;
#9521=ADVANCED_FACE ( 'NONE', ( #14410 ), #2808, .F. ) ;
#9529=CARTESIAN_POINT ( 'NONE',  ( 30.99999999999997513, 0.000000000000000000, 25.99999999999999645 ) ) ;
#9530=DIRECTION ( 'NONE',  ( 0.000000000000000000, 1.000000000000000000, 0.000000000000000000 ) ) ;
#9544=DIRECTION ( 'NONE',  ( 0.000000000000000000, 1.000000000000000000, 0.000000000000000000 ) ) ;
#9545=PLANE ( 'NONE',  #2905 ) ;
#9566=CARTESIAN_POINT ( 'NONE',  ( -26.00000000000002132, 10.00000000000000000, 40.00000000000000711 ) ) ;
#9584=DIRECTION ( 'NONE',  ( -0.000000000000000000, -1.000000000000000000, -0.000000000000000000 ) ) ;
#9601=EDGE_CURVE ( 'NONE', #16504, #13507, #7779, .T. ) ;
#9604=DIRECTION ( 'NONE',  ( 0.000000000000000000, -0.000000000000000000, 1.000000000000000000 ) ) ;
#9613=DIRECTION ( 'NONE',  ( -0.000000000000000000, -0.000000000000000000, 1.000000000000000000 ) ) ;
#9619=DIRECTION ( 'NONE',  ( -0.000000000000000000, 1.000000000000000000, -0.000000000000000000 ) ) ;
#9620=AXIS2_PLACEMENT_3D ( 'NONE', #9861, #10030, #510 ) ;
#9643=ORIENTED_EDGE ( 'NONE', *, *, #9488, .T. ) ;
#9678=AXIS2_PLACEMENT_3D ( 'NONE', #1170, #16879, #7767 ) ;
#9703=AXIS2_PLACEMENT_3D ( 'NONE', #244, #5729, #1438 ) ;
#9714=AXIS2_PLACEMENT_3D ( 'NONE', #15762, #13192, #15596 ) ;
#9719=DIRECTION ( 'NONE',  ( -0.000000000000000000, -1.000000000000000000, -0.000000000000000000 ) ) ;
#9722=CARTESIAN_POINT ( 'NONE',  ( -32.00000000000000711, 10.00000000000000000, -22.00000000000000355 ) ) ;
#9735=ADVANCED_FACE ( 'NONE', ( #4188 ), #14838, .F. ) ;
#9741=DIRECTION ( 'NONE',  ( 0.000000000000000000, 0.000000000000000000, -1.000000000000000000 ) ) ;
#9751=ORIENTED_EDGE ( 'NONE', *, *, #10628, .F. ) ;
#9755=PLANE ( 'NONE',  #10775 ) ;
#9757=ORIENTED_EDGE ( 'NONE', *, *, #15377, .T. ) ;
#9768=VERTEX_POINT ( 'NONE', #2109 ) ;
#9771=VECTOR ( 'NONE', #1408, 1000.000000000000000 ) ;
#9773=DIRECTION ( 'NONE',  ( 1.000000000000000000, 0.000000000000000000, 0.000000000000000000 ) ) ;
#9775=ORIENTED_EDGE ( 'NONE', *, *, #8155, .F. ) ;
#9795=DIRECTION ( 'NONE',  ( -1.000000000000000000, 0.000000000000000000, -3.854941057726246479E-16 ) ) ;
#9811=EDGE_CURVE ( 'NONE', #3550, #5229, #16453, .T. ) ;
#9832=VERTEX_POINT ( 'NONE', #2025 ) ;
#9834=AXIS2_PLACEMENT_3D ( 'NONE', #4916, #8883, #12575 ) ;
#9840=CARTESIAN_POINT ( 'NONE',  ( -33.00000000000000000, 8.000000000000000000, -26.00000000000000355 ) ) ;
#9842=ORIENTED_EDGE ( 'NONE', *, *, #13099, .F. ) ;
#9853=ORIENTED_EDGE ( 'NONE', *, *, #11101, .T. ) ;
#9861=CARTESIAN_POINT ( 'NONE',  ( 31.00000000000001421, 10.00000000000000000, 22.99999999999999645 ) ) ;
#9864=VECTOR ( 'NONE', #14399, 1000.000000000000000 ) ;
#9871=PLANE ( 'NONE',  #13528 ) ;
#9872=VECTOR ( 'NONE', #13984, 1000.000000000000000 ) ;
#9897=ORIENTED_EDGE ( 'NONE', *, *, #1858, .F. ) ;
#9900=VERTEX_POINT ( 'NONE', #6549 ) ;
#9906=ADVANCED_FACE ( 'NONE', ( #2528 ), #16783, .T. ) ;
#9922=FACE_OUTER_BOUND ( 'NONE', #14573, .T. ) ;
#9940=EDGE_CURVE ( 'NONE', #4506, #14978, #6886, .T. ) ;
#9944=CARTESIAN_POINT ( 'NONE',  ( -22.00000000000001776, 10.00000000000000000, 33.00000000000000711 ) ) ;
#9955=VERTEX_POINT ( 'NONE', #1249 ) ;
#9956=DIRECTION ( 'NONE',  ( 3.854941057726246479E-16, 0.000000000000000000, -1.000000000000000000 ) ) ;
#9962=ORIENTED_EDGE ( 'NONE', *, *, #2364, .T. ) ;
#9963=CYLINDRICAL_SURFACE ( 'NONE', #2580, 5.000000000000000888 ) ;
#9968=ORIENTED_EDGE ( 'NONE', *, *, #8352, .T. ) ;
#9974=CARTESIAN_POINT ( 'NONE',  ( -22.00000000000001776, 6.000000000000000000, 32.00000000000000711 ) ) ;
#9983=DIRECTION ( 'NONE',  ( 1.000000000000000000, 0.000000000000000000, 0.000000000000000000 ) ) ;
#10008=FACE_OUTER_BOUND ( 'NONE', #14226, .T. ) ;
#10010=ORIENTED_EDGE ( 'NONE', *, *, #15649, .F. ) ;
#10011=DIRECTION ( 'NONE',  ( -1.000000000000000000, -0.000000000000000000, -0.000000000000000000 ) ) ;
#10024=ORIENTED_EDGE ( 'NONE', *, *, #12363, .T. ) ;
#10030=DIRECTION ( 'NONE',  ( 0.000000000000000000, 0.000000000000000000, -1.000000000000000000 ) ) ;
#10035=CARTESIAN_POINT ( 'NONE',  ( 31.00000000000001776, 0.000000000000000000, -25.99999999999999645 ) ) ;
#10038=ADVANCED_FACE ( 'NONE', ( #14297 ), #5178, .T. ) ;
#10043=FACE_OUTER_BOUND ( 'NONE', #4741, .T. ) ;
#10047=ORIENTED_EDGE ( 'NONE', *, *, #3803, .T. ) ;
#10049=CARTESIAN_POINT ( 'NONE',  ( -40.00000000000000711, 10.00000000000000000, 26.00000000000000000 ) ) ;
#10051=EDGE_LOOP ( 'NONE', ( #9107, #3535, #15057, #11754, #10912, #11602 ) ) ;
#10052=VECTOR ( 'NONE', #14789, 1000.000000000000000 ) ;
#10063=SHAPE_DEFINITION_REPRESENTATION ( #6553, #25 ) ;
#10067=VERTEX_POINT ( 'NONE', #11031 ) ;
#10077=ORIENTED_EDGE ( 'NONE', *, *, #477, .F. ) ;
#10079=ORIENTED_EDGE ( 'NONE', *, *, #5842, .F. ) ;
#10083=CARTESIAN_POINT ( 'NONE',  ( -26.00000000000002132, 10.00000000000000000, -31.00000000000003553 ) ) ;
#10090=DIRECTION ( 'NONE',  ( -0.000000000000000000, 0.000000000000000000, 1.000000000000000000 ) ) ;
#10092=ORIENTED_EDGE ( 'NONE', *, *, #10168, .F. ) ;
#10096=ORIENTED_EDGE ( 'NONE', *, *, #14571, .T. ) ;
#10103=DIRECTION ( 'NONE',  ( 0.000000000000000000, 1.000000000000000000, 0.000000000000000000 ) ) ;
#10115=CARTESIAN_POINT ( 'NONE',  ( -31.00000000000002132, 10.00000000000000000, -31.00000000000000000 ) ) ;
#10118=PLANE ( 'NONE',  #4700 ) ;
#10125=AXIS2_PLACEMENT_3D ( 'NONE', #8819, #15520, #3671 ) ;
#10127=ORIENTED_EDGE ( 'NONE', *, *, #7160, .T. ) ;
#10135=CARTESIAN_POINT ( 'NONE',  ( -26.00000000000001776, 10.00000000000000000, 31.00000000000003553 ) ) ;
#10142=LINE ( 'NONE', #6570, #1380 ) ;
#10151=EDGE_CURVE ( 'NONE', #6355, #1812, #9499, .T. ) ;
#10153=ORIENTED_EDGE ( 'NONE', *, *, #11101, .F. ) ;
#10157=ORIENTED_EDGE ( 'NONE', *, *, #6686, .F. ) ;
#10162=ORIENTED_EDGE ( 'NONE', *, *, #11613, .F. ) ;
#10168=EDGE_CURVE ( 'NONE', #10736, #11828, #8716, .T. ) ;
#10175=ORIENTED_EDGE ( 'NONE', *, *, #463, .F. ) ;
#10183=( NAMED_UNIT ( * ) PLANE_ANGLE_UNIT ( ) SI_UNIT ( $, .RADIAN. ) );
#10200=DIRECTION ( 'NONE',  ( -1.000000000000000000, -0.000000000000000000, -0.000000000000000000 ) ) ;
#10209=DIRECTION ( 'NONE',  ( 0.000000000000000000, 0.000000000000000000, -1.000000000000000000 ) ) ;
#10210=ORIENTED_EDGE ( 'NONE', *, *, #13017, .T. ) ;
#10227=CARTESIAN_POINT ( 'NONE',  ( 18.99999999999998224, 8.000000000000000000, -35.99999999999999289 ) ) ;
#10231=CARTESIAN_POINT ( 'NONE',  ( 25.99999999999997868, 0.000000000000000000, 40.00000000000000711 ) ) ;
#10249=ORIENTED_EDGE ( 'NONE', *, *, #10444, .T. ) ;
#10250=AXIS2_PLACEMENT_3D ( 'NONE', #15225, #11182, #16416 ) ;
#10252=LINE ( 'NONE', #11614, #1966 ) ;
#10260=DIRECTION ( 'NONE',  ( -0.000000000000000000, -0.000000000000000000, 1.000000000000000000 ) ) ;
#10263=VERTEX_POINT ( 'NONE', #11447 ) ;
#10280=DIRECTION ( 'NONE',  ( 1.000000000000000000, 0.000000000000000000, -0.000000000000000000 ) ) ;
#10291=CARTESIAN_POINT ( 'NONE',  ( 36.99999999999999289, 10.00000000000000000, 22.99999999999999645 ) ) ;
#10297=VERTEX_POINT ( 'NONE', #2003 ) ;
#10300=ORIENTED_EDGE ( 'NONE', *, *, #9068, .T. ) ;
#10301=PLANE ( 'NONE',  #15208 ) ;
#10302=CARTESIAN_POINT ( 'NONE',  ( 25.99999999999998224, 10.00000000000000000, -31.99999999999998579 ) ) ;
#10303=DIRECTION ( 'NONE',  ( -1.000000000000000000, 0.000000000000000000, 0.000000000000000000 ) ) ;
#10317=DIRECTION ( 'NONE',  ( 0.000000000000000000, 0.000000000000000000, 1.000000000000000000 ) ) ;
#10327=LINE ( 'NONE', #14109, #4770 ) ;
#10339=DIRECTION ( 'NONE',  ( -1.000000000000000000, 0.000000000000000000, 0.000000000000000000 ) ) ;
#10348=CARTESIAN_POINT ( 'NONE',  ( -37.00000000000000711, 0.000000000000000000, -23.00000000000000000 ) ) ;
#10371=DIRECTION ( 'NONE',  ( -1.000000000000000000, 0.000000000000000000, -0.000000000000000000 ) ) ;
#10374=VERTEX_POINT ( 'NONE', #7569 ) ;
#10381=ORIENTED_EDGE ( 'NONE', *, *, #13187, .T. ) ;
#10399=EDGE_LOOP ( 'NONE', ( #12045, #413, #14886, #5646, #10381, #8556 ) ) ;
#10416=CARTESIAN_POINT ( 'NONE',  ( -22.00000000000001776, 8.000000000000000000, 33.00000000000000711 ) ) ;
#10420=DIRECTION ( 'NONE',  ( -0.000000000000000000, -1.000000000000000000, -0.000000000000000000 ) ) ;
#10427=AXIS2_PLACEMENT_3D ( 'NONE', #6424, #7552, #5224 ) ;
#10444=EDGE_CURVE ( 'NONE', #8527, #1812, #10252, .T. ) ;
#10455=DIRECTION ( 'NONE',  ( 1.000000000000000000, 0.000000000000000000, 0.000000000000000000 ) ) ;
#10459=DIRECTION ( 'NONE',  ( -0.000000000000000000, 1.000000000000000000, -0.000000000000000000 ) ) ;
#10466=DIRECTION ( 'NONE',  ( -3.854941057726255847E-16, -0.000000000000000000, 1.000000000000000000 ) ) ;
#10468=VERTEX_POINT ( 'NONE', #3030 ) ;
#10470=STYLED_ITEM ( 'NONE', ( #3574 ), #14111 ) ;
#10484=CYLINDRICAL_SURFACE ( 'NONE', #16614, 3.000000000000002665 ) ;
#10488=VERTEX_POINT ( 'NONE', #15989 ) ;
#10499=CIRCLE ( 'NONE', #16529, 2.999999999999995559 ) ;
#10515=ORIENTED_EDGE ( 'NONE', *, *, #13983, .T. ) ;
#10518=VECTOR ( 'NONE', #16679, 1000.000000000000000 ) ;
#10520=CARTESIAN_POINT ( 'NONE',  ( 25.99999999999997868, 8.000000000000000000, -39.99999999999999289 ) ) ;
#10528=LINE ( 'NONE', #15765, #11442 ) ;
#10534=DIRECTION ( 'NONE',  ( 0.000000000000000000, 0.000000000000000000, 1.000000000000000000 ) ) ;
#10546=FACE_OUTER_BOUND ( 'NONE', #16523, .T. ) ;
#10548=VERTEX_POINT ( 'NONE', #11966 ) ;
#10551=AXIS2_PLACEMENT_3D ( 'NONE', #11400, #14155, #10371 ) ;
#10554=ORIENTED_EDGE ( 'NONE', *, *, #6958, .F. ) ;
#10556=ADVANCED_FACE ( 'NONE', ( #1651 ), #5687, .T. ) ;
#10557=DIRECTION ( 'NONE',  ( 0.000000000000000000, 0.000000000000000000, -1.000000000000000000 ) ) ;
#10564=ORIENTED_EDGE ( 'NONE', *, *, #12600, .T. ) ;
#10567=CARTESIAN_POINT ( 'NONE',  ( -37.00000000000000711, 10.00000000000000000, 23.00000000000000000 ) ) ;
#10570=EDGE_CURVE ( 'NONE', #6355, #14833, #15404, .T. ) ;
#10573=ORIENTED_EDGE ( 'NONE', *, *, #6342, .F. ) ;
#10576=EDGE_CURVE ( 'NONE', #8527, #9305, #7126, .T. ) ;
#10579=CARTESIAN_POINT ( 'NONE',  ( -26.00000000000002132, 10.00000000000000000, -31.00000000000003553 ) ) ;
#10588=DIRECTION ( 'NONE',  ( 0.000000000000000000, 0.000000000000000000, -1.000000000000000000 ) ) ;
#10589=CARTESIAN_POINT ( 'NONE',  ( -26.00000000000002132, 10.00000000000000000, 40.00000000000000711 ) ) ;
#10591=CARTESIAN_POINT ( 'NONE',  ( 36.99999999999999289, 10.00000000000000000, 17.99999999999998934 ) ) ;
#10600=CIRCLE ( 'NONE', #8123, 4.000000000000007105 ) ;
#10606=CARTESIAN_POINT ( 'NONE',  ( -37.00000000000000711, 10.00000000000000000, -23.00000000000000000 ) ) ;
#10610=VECTOR ( 'NONE', #15246, 1000.000000000000000 ) ;
#10615=EDGE_CURVE ( 'NONE', #1299, #529, #11179, .T. ) ;
#10626=DIRECTION ( 'NONE',  ( 0.000000000000000000, 0.000000000000000000, -1.000000000000000000 ) ) ;
#10628=EDGE_CURVE ( 'NONE', #14978, #1977, #16587, .T. ) ;
#10629=ORIENTED_EDGE ( 'NONE', *, *, #3634, .F. ) ;
#10632=DIRECTION ( 'NONE',  ( 0.000000000000000000, -1.000000000000000000, 0.000000000000000000 ) ) ;
#10633=VERTEX_POINT ( 'NONE', #3368 ) ;
#10636=DIRECTION ( 'NONE',  ( 0.000000000000000000, 0.000000000000000000, 1.000000000000000000 ) ) ;
#10646=ORIENTED_EDGE ( 'NONE', *, *, #9515, .F. ) ;
#10649=DIRECTION ( 'NONE',  ( -0.000000000000000000, 1.000000000000000000, -0.000000000000000000 ) ) ;
#10650=LINE ( 'NONE', #4705, #1005 ) ;
#10659=LINE ( 'NONE', #15982, #14110 ) ;
#10677=CARTESIAN_POINT ( 'NONE',  ( -37.00000000000000711, 10.00000000000000000, 23.00000000000000000 ) ) ;
#10681=EDGE_LOOP ( 'NONE', ( #11847, #800, #9297, #11832 ) ) ;
#10698=CYLINDRICAL_SURFACE ( 'NONE', #10769, 5.000000000000000888 ) ;
#10700=CARTESIAN_POINT ( 'NONE',  ( -40.00000000000000711, 10.00000000000000000, -19.00000000000000355 ) ) ;
#10704=ORIENTED_EDGE ( 'NONE', *, *, #7062, .F. ) ;
#10712=DIRECTION ( 'NONE',  ( 1.000000000000000000, -0.000000000000000000, 0.000000000000000000 ) ) ;
#10717=DIRECTION ( 'NONE',  ( -0.000000000000000000, -1.000000000000000000, -0.000000000000000000 ) ) ;
#10734=CARTESIAN_POINT ( 'NONE',  ( -26.00000000000001776, 10.00000000000000000, 31.00000000000003553 ) ) ;
#10736=VERTEX_POINT ( 'NONE', #4487 ) ;
#10737=AXIS2_PLACEMENT_3D ( 'NONE', #9268, #16811, #1105 ) ;
#10749=ORIENTED_EDGE ( 'NONE', *, *, #2149, .T. ) ;
#10751=AXIS2_PLACEMENT_3D ( 'NONE', #10606, #13106, #14649 ) ;
#10753=DIRECTION ( 'NONE',  ( -3.854941057726249437E-16, -0.000000000000000000, 1.000000000000000000 ) ) ;
#10769=AXIS2_PLACEMENT_3D ( 'NONE', #5541, #13547, #4176 ) ;
#10772=ORIENTED_EDGE ( 'NONE', *, *, #14412, .T. ) ;
#10773=CARTESIAN_POINT ( 'NONE',  ( -31.00000000000001776, 10.00000000000000000, 31.00000000000000000 ) ) ;
#10775=AXIS2_PLACEMENT_3D ( 'NONE', #14071, #14245, #9085 ) ;
#10777=CARTESIAN_POINT ( 'NONE',  ( -37.00000000000000711, 6.000000000000000000, -23.00000000000000000 ) ) ;
#10794=ORIENTED_EDGE ( 'NONE', *, *, #14231, .T. ) ;
#10805=EDGE_CURVE ( 'NONE', #11864, #14282, #15554, .T. ) ;
#10823=CARTESIAN_POINT ( 'NONE',  ( -23.00000000000002842, 0.000000000000000000, -31.00000000000003553 ) ) ;
#10824=VERTEX_POINT ( 'NONE', #10227 ) ;
#10829=CARTESIAN_POINT ( 'NONE',  ( 25.99999999999998224, 10.00000000000000000, -31.00000000000003197 ) ) ;
#10830=ORIENTED_EDGE ( 'NONE', *, *, #14412, .F. ) ;
#10835=EDGE_LOOP ( 'NONE', ( #16753, #16706, #1440, #2778 ) ) ;
#10851=DIRECTION ( 'NONE',  ( -0.000000000000000000, -1.000000000000000000, -0.000000000000000000 ) ) ;
#10863=AXIS2_PLACEMENT_3D ( 'NONE', #10773, #6806, #13362 ) ;
#10876=CARTESIAN_POINT ( 'NONE',  ( 32.99999999999998579, 10.00000000000000000, 25.99999999999999645 ) ) ;
#10883=ORIENTED_EDGE ( 'NONE', *, *, #11870, .F. ) ;
#10885=EDGE_CURVE ( 'NONE', #5706, #14554, #14859, .T. ) ;
#10894=EDGE_LOOP ( 'NONE', ( #9466, #6863, #847, #554 ) ) ;
#10897=PLANE ( 'NONE',  #6739 ) ;
#10907=ORIENTED_EDGE ( 'NONE', *, *, #14552, .T. ) ;
#10912=ORIENTED_EDGE ( 'NONE', *, *, #281, .T. ) ;
#10915=EDGE_LOOP ( 'NONE', ( #16164, #804, #6977, #4826 ) ) ;
#10921=ORIENTED_EDGE ( 'NONE', *, *, #16269, .T. ) ;
#10934=CARTESIAN_POINT ( 'NONE',  ( 31.00000000000001421, 10.00000000000000000, 22.99999999999999645 ) ) ;
#10936=CARTESIAN_POINT ( 'NONE',  ( -31.00000000000005684, 10.00000000000000000, -23.00000000000000000 ) ) ;
#10947=VERTEX_POINT ( 'NONE', #8162 ) ;
#10953=PLANE ( 'NONE',  #16505 ) ;
#10960=DIRECTION ( 'NONE',  ( 0.000000000000000000, 0.000000000000000000, -1.000000000000000000 ) ) ;
#10969=DIRECTION ( 'NONE',  ( -0.000000000000000000, -1.000000000000000000, -0.000000000000000000 ) ) ;
#10978=LINE ( 'NONE', #13569, #2796 ) ;
#11010=CARTESIAN_POINT ( 'NONE',  ( -33.00000000000000000, 10.00000000000000000, -26.00000000000000355 ) ) ;
#11023=AXIS2_PLACEMENT_3D ( 'NONE', #2945, #6712, #12047 ) ;
#11027=COLOUR_RGB ( '', 0.31764706, 0.68627451, 0.89019608) ;
#11031=CARTESIAN_POINT ( 'NONE',  ( 36.99999999999999289, 10.00000000000000000, 17.99999999999998934 ) ) ;
#11042=CARTESIAN_POINT ( 'NONE',  ( -36.00000000000000711, 8.000000000000000000, -22.00000000000000355 ) ) ;
#11047=CIRCLE ( 'NONE', #5260, 4.999999999999997335 ) ;
#11050=AXIS2_PLACEMENT_3D ( 'NONE', #11042, #13787, #4755 ) ;
#11051=VECTOR ( 'NONE', #16314, 1000.000000000000000 ) ;
#11062=LINE ( 'NONE', #3502, #13770 ) ;
#11070=CARTESIAN_POINT ( 'NONE',  ( 31.00000000000001421, 10.00000000000000000, 25.99999999999999645 ) ) ;
#11072=PLANE ( 'NONE',  #1451 ) ;
#11095=VECTOR ( 'NONE', #1732, 1000.000000000000000 ) ;
#11101=EDGE_CURVE ( 'NONE', #10468, #13251, #16318, .T. ) ;
#11123=DIRECTION ( 'NONE',  ( 0.000000000000000000, 1.000000000000000000, 0.000000000000000000 ) ) ;
#11130=CARTESIAN_POINT ( 'NONE',  ( -26.00000000000002132, 10.00000000000000000, -31.00000000000003553 ) ) ;
#11133=CARTESIAN_POINT ( 'NONE',  ( 35.99999999999999289, 8.000000000000000000, 18.99999999999999289 ) ) ;
#11135=ADVANCED_FACE ( 'NONE', ( #16396 ), #9755, .F. ) ;
#11141=EDGE_CURVE ( 'NONE', #10824, #7385, #10499, .T. ) ;
#11157=ORIENTED_EDGE ( 'NONE', *, *, #14552, .F. ) ;
#11159=LINE ( 'NONE', #8832, #2532 ) ;
#11165=AXIS2_PLACEMENT_3D ( 'NONE', #15633, #9209, #14444 ) ;
#11170=EDGE_CURVE ( 'NONE', #3203, #13507, #3597, .T. ) ;
#11178=ORIENTED_EDGE ( 'NONE', *, *, #782, .F. ) ;
#11179=LINE ( 'NONE', #14970, #12393 ) ;
#11182=DIRECTION ( 'NONE',  ( -0.000000000000000000, -1.000000000000000000, 0.000000000000000000 ) ) ;
#11212=CARTESIAN_POINT ( 'NONE',  ( -40.00000000000000711, 10.00000000000000000, 26.00000000000000000 ) ) ;
#11213=ORIENTED_EDGE ( 'NONE', *, *, #6032, .F. ) ;
#11216=EDGE_CURVE ( 'NONE', #4234, #10468, #11047, .T. ) ;
#11221=ORIENTED_EDGE ( 'NONE', *, *, #1107, .F. ) ;
#11225=ORIENTED_EDGE ( 'NONE', *, *, #13099, .T. ) ;
#11230=DIRECTION ( 'NONE',  ( -0.000000000000000000, 1.000000000000000000, -0.000000000000000000 ) ) ;
#11266=ORIENTED_EDGE ( 'NONE', *, *, #5311, .F. ) ;
#11271=EDGE_LOOP ( 'NONE', ( #2766, #13343, #10646, #6290 ) ) ;
#11278=CARTESIAN_POINT ( 'NONE',  ( -40.00000000000000711, 10.00000000000000000, -18.00000000000000355 ) ) ;
#11287=DIRECTION ( 'NONE',  ( 0.000000000000000000, -1.000000000000000000, 0.000000000000000000 ) ) ;
#11289=LINE ( 'NONE', #11212, #13724 ) ;
#11309=DIRECTION ( 'NONE',  ( 0.000000000000000000, 0.000000000000000000, -1.000000000000000000 ) ) ;
#11310=VECTOR ( 'NONE', #11848, 1000.000000000000000 ) ;
#11312=CARTESIAN_POINT ( 'NONE',  ( -31.00000000000005329, 10.00000000000000000, 26.00000000000000000 ) ) ;
#11316=CARTESIAN_POINT ( 'NONE',  ( 35.99999999999999289, 8.000000000000000000, 18.99999999999999289 ) ) ;
#11319=AXIS2_PLACEMENT_3D ( 'NONE', #14502, #2723, #7957 ) ;
#11324=DIRECTION ( 'NONE',  ( -0.000000000000000000, -1.000000000000000000, -0.000000000000000000 ) ) ;
#11325=VECTOR ( 'NONE', #15409, 1000.000000000000000 ) ;
#11326=CIRCLE ( 'NONE', #9703, 5.000000000000000888 ) ;
#11336=CARTESIAN_POINT ( 'NONE',  ( -26.00000000000002132, 0.000000000000000000, -31.00000000000003553 ) ) ;
#11338=CIRCLE ( 'NONE', #15998, 5.000000000000000888 ) ;
#11352=VERTEX_POINT ( 'NONE', #2811 ) ;
#11370=DIRECTION ( 'NONE',  ( -1.000000000000000000, 0.000000000000000000, 3.854941057726249930E-16 ) ) ;
#11371=LINE ( 'NONE', #4842, #15337 ) ;
#11373=VERTEX_POINT ( 'NONE', #5648 ) ;
#11375=DIRECTION ( 'NONE',  ( 0.000000000000000000, -0.000000000000000000, -1.000000000000000000 ) ) ;
#11379=VERTEX_POINT ( 'NONE', #1532 ) ;
#11383=ORIENTED_EDGE ( 'NONE', *, *, #11170, .F. ) ;
#11386=DIRECTION ( 'NONE',  ( 0.000000000000000000, 0.000000000000000000, 1.000000000000000000 ) ) ;
#11393=CARTESIAN_POINT ( 'NONE',  ( -18.00000000000001421, 6.000000000000000000, 36.00000000000000711 ) ) ;
#11400=CARTESIAN_POINT ( 'NONE',  ( -26.00000000000002132, 10.00000000000000000, 40.00000000000000711 ) ) ;
#11401=LINE ( 'NONE', #846, #6502 ) ;
#11427=ADVANCED_FACE ( 'NONE', ( #10546 ), #15779, .F. ) ;
#11442=VECTOR ( 'NONE', #8205, 1000.000000000000000 ) ;
#11447=CARTESIAN_POINT ( 'NONE',  ( 36.99999999999999289, 6.000000000000000000, 22.99999999999999645 ) ) ;
#11449=VECTOR ( 'NONE', #10466, 1000.000000000000000 ) ;
#11452=DIRECTION ( 'NONE',  ( -0.000000000000000000, -1.000000000000000000, -0.000000000000000000 ) ) ;
#11455=ORIENTED_EDGE ( 'NONE', *, *, #10615, .T. ) ;
#11457=CARTESIAN_POINT ( 'NONE',  ( -23.00000000000002132, 6.000000000000000000, 37.00000000000000711 ) ) ;
#11489=DIRECTION ( 'NONE',  ( 0.000000000000000000, -0.000000000000000000, 1.000000000000000000 ) ) ;
#11492=EDGE_CURVE ( 'NONE', #14833, #10736, #15402, .T. ) ;
#11496=EDGE_CURVE ( 'NONE', #2454, #1299, #2273, .T. ) ;
#11509=LINE ( 'NONE', #4976, #8232 ) ;
#11513=CARTESIAN_POINT ( 'NONE',  ( 25.99999999999997868, 8.000000000000000000, -39.99999999999999289 ) ) ;
#11520=ORIENTED_EDGE ( 'NONE', *, *, #8483, .F. ) ;
#11556=CARTESIAN_POINT ( 'NONE',  ( -22.00000000000001776, 8.000000000000000000, 33.00000000000000711 ) ) ;
#11566=FACE_OUTER_BOUND ( 'NONE', #13529, .T. ) ;
#11573=CARTESIAN_POINT ( 'NONE',  ( -23.00000000000002132, 0.000000000000000000, 37.00000000000000711 ) ) ;
#11590=EDGE_CURVE ( 'NONE', #3569, #2956, #5164, .T. ) ;
#11602=ORIENTED_EDGE ( 'NONE', *, *, #12447, .F. ) ;
#11604=CARTESIAN_POINT ( 'NONE',  ( 39.99999999999999289, 0.000000000000000000, -26.00000000000000000 ) ) ;
#11605=VECTOR ( 'NONE', #9584, 1000.000000000000000 ) ;
#11613=EDGE_CURVE ( 'NONE', #14988, #14016, #6616, .T. ) ;
#11614=CARTESIAN_POINT ( 'NONE',  ( -18.00000000000001421, 10.00000000000000000, 40.00000000000000711 ) ) ;
#11630=CARTESIAN_POINT ( 'NONE',  ( 22.99999999999997513, 10.00000000000000000, 31.00000000000005684 ) ) ;
#11647=FACE_OUTER_BOUND ( 'NONE', #3266, .T. ) ;
#11655=LINE ( 'NONE', #8827, #12776 ) ;
#11663=FACE_OUTER_BOUND ( 'NONE', #10681, .T. ) ;
#11666=CYLINDRICAL_SURFACE ( 'NONE', #1056, 3.999999999999996447 ) ;
#11667=PLANE ( 'NONE',  #6180 ) ;
#11679=CARTESIAN_POINT ( 'NONE',  ( 31.00000000000001421, 6.000000000000000000, 22.99999999999999645 ) ) ;
#11680=VERTEX_POINT ( 'NONE', #3989 ) ;
#11684=EDGE_CURVE ( 'NONE', #2977, #10067, #14540, .T. ) ;
#11685=CARTESIAN_POINT ( 'NONE',  ( -22.00000000000001776, 10.00000000000000000, 36.00000000000000711 ) ) ;
#11694=EDGE_CURVE ( 'NONE', #3043, #8801, #13258, .T. ) ;
#11698=CIRCLE ( 'NONE', #6765, 8.000000000000000000 ) ;
#11710=EDGE_CURVE ( 'NONE', #13693, #16255, #14205, .T. ) ;
#11717=EDGE_CURVE ( 'NONE', #5545, #3569, #12169, .T. ) ;
#11718=CARTESIAN_POINT ( 'NONE',  ( 22.99999999999998224, 0.000000000000000000, -36.99999999999999289 ) ) ;
#11721=ORIENTED_EDGE ( 'NONE', *, *, #9068, .F. ) ;
#11724=( LENGTH_UNIT ( ) NAMED_UNIT ( * ) SI_UNIT ( .MILLI., .METRE. ) );
#11754=ORIENTED_EDGE ( 'NONE', *, *, #12878, .T. ) ;
#11763=VERTEX_POINT ( 'NONE', #10934 ) ;
#11784=VECTOR ( 'NONE', #2890, 1000.000000000000000 ) ;
#11791=CARTESIAN_POINT ( 'NONE',  ( 18.99999999999998224, 8.000000000000000000, -35.99999999999999289 ) ) ;
#11804=DIRECTION ( 'NONE',  ( 0.000000000000000000, 0.000000000000000000, 1.000000000000000000 ) ) ;
#11818=CARTESIAN_POINT ( 'NONE',  ( 18.99999999999998224, 10.00000000000000000, -35.99999999999999289 ) ) ;
#11828=VERTEX_POINT ( 'NONE', #9387 ) ;
#11832=ORIENTED_EDGE ( 'NONE', *, *, #12447, .T. ) ;
#11847=ORIENTED_EDGE ( 'NONE', *, *, #10805, .T. ) ;
#11848=DIRECTION ( 'NONE',  ( -0.000000000000000000, -1.000000000000000000, -0.000000000000000000 ) ) ;
#11864=VERTEX_POINT ( 'NONE', #2858 ) ;
#11870=EDGE_CURVE ( 'NONE', #14554, #9955, #8863, .T. ) ;
#11888=DIRECTION ( 'NONE',  ( 1.000000000000000000, -0.000000000000000000, 0.000000000000000000 ) ) ;
#11896=AXIS2_PLACEMENT_3D ( 'NONE', #8717, #15239, #13952 ) ;
#11899=ORIENTED_EDGE ( 'NONE', *, *, #5247, .F. ) ;
#11920=DIRECTION ( 'NONE',  ( 3.854941057726247958E-16, -0.000000000000000000, 1.000000000000000000 ) ) ;
#11921=ORIENTED_EDGE ( 'NONE', *, *, #5085, .F. ) ;
#11925=DIRECTION ( 'NONE',  ( 0.000000000000000000, 1.000000000000000000, 0.000000000000000000 ) ) ;
#11932=CARTESIAN_POINT ( 'NONE',  ( 25.99999999999997868, 10.00000000000000000, 40.00000000000000711 ) ) ;
#11935=VERTEX_POINT ( 'NONE', #12557 ) ;
#11939=CARTESIAN_POINT ( 'NONE',  ( 31.00000000000001776, 10.00000000000000000, -25.99999999999999645 ) ) ;
#11953=ORIENTED_EDGE ( 'NONE', *, *, #6439, .T. ) ;
#11966=CARTESIAN_POINT ( 'NONE',  ( 25.99999999999997868, 10.00000000000000000, 40.00000000000000711 ) ) ;
#11970=EDGE_CURVE ( 'NONE', #2956, #15552, #4901, .T. ) ;
#11973=CARTESIAN_POINT ( 'NONE',  ( 35.99999999999999289, 6.000000000000000000, 21.99999999999999645 ) ) ;
#12004=ADVANCED_FACE ( 'NONE', ( #964 ), #3371, .T. ) ;
#12016=DIRECTION ( 'NONE',  ( -3.854941057726249437E-16, 0.000000000000000000, -1.000000000000000000 ) ) ;
#12018=CARTESIAN_POINT ( 'NONE',  ( -32.00000000000000711, 6.000000000000000000, -22.00000000000000355 ) ) ;
#12028=EDGE_CURVE ( 'NONE', #4908, #4138, #2283, .T. ) ;
#12040=CARTESIAN_POINT ( 'NONE',  ( 25.99999999999998224, 8.000000000000000000, -32.99999999999999289 ) ) ;
#12045=ORIENTED_EDGE ( 'NONE', *, *, #16332, .F. ) ;
#12047=DIRECTION ( 'NONE',  ( 0.000000000000000000, 0.000000000000000000, 1.000000000000000000 ) ) ;
#12051=VERTEX_POINT ( 'NONE', #12979 ) ;
#12069=DIRECTION ( 'NONE',  ( -1.000000000000000000, 0.000000000000000000, 0.000000000000000000 ) ) ;
#12082=CARTESIAN_POINT ( 'NONE',  ( -19.00000000000001776, 10.00000000000000000, 36.00000000000000711 ) ) ;
#12084=ORIENTED_EDGE ( 'NONE', *, *, #11216, .T. ) ;
#12088=CARTESIAN_POINT ( 'NONE',  ( 25.99999999999998224, 10.00000000000000000, -31.00000000000003197 ) ) ;
#12090=VERTEX_POINT ( 'NONE', #10231 ) ;
#12092=CARTESIAN_POINT ( 'NONE',  ( -40.00000000000000711, 10.00000000000000000, -19.00000000000000355 ) ) ;
#12101=CARTESIAN_POINT ( 'NONE',  ( -31.00000000000005329, 10.00000000000000000, 26.00000000000000000 ) ) ;
#12125=ORIENTED_EDGE ( 'NONE', *, *, #231, .F. ) ;
#12132=VECTOR ( 'NONE', #5365, 1000.000000000000000 ) ;
#12136=ORIENTED_EDGE ( 'NONE', *, *, #2364, .F. ) ;
#12147=AXIS2_PLACEMENT_3D ( 'NONE', #13823, #13985, #936 ) ;
#12157=LINE ( 'NONE', #10777, #12680 ) ;
#12160=CARTESIAN_POINT ( 'NONE',  ( -22.00000000000001776, 6.000000000000000000, 32.00000000000000711 ) ) ;
#12168=DIRECTION ( 'NONE',  ( -3.854941057726249437E-16, 0.000000000000000000, -1.000000000000000000 ) ) ;
#12169=CIRCLE ( 'NONE', #372, 2.999999999999995559 ) ;
#12176=AXIS2_PLACEMENT_3D ( 'NONE', #2790, #5627, #4169 ) ;
#12178=CARTESIAN_POINT ( 'NONE',  ( 31.99999999999998579, 6.000000000000000000, 21.99999999999999645 ) ) ;
#12182=ORIENTED_EDGE ( 'NONE', *, *, #8896, .F. ) ;
#12185=FACE_BOUND ( 'NONE', #5698, .T. ) ;
#12187=LINE ( 'NONE', #6836, #1097 ) ;
#12226=VECTOR ( 'NONE', #5376, 1000.000000000000000 ) ;
#12247=CARTESIAN_POINT ( 'NONE',  ( -36.00000000000000711, 8.000000000000000000, -19.00000000000000000 ) ) ;
#12256=CARTESIAN_POINT ( 'NONE',  ( 39.99999999999999289, 10.00000000000000000, -26.00000000000000000 ) ) ;
#12260=DIRECTION ( 'NONE',  ( -1.000000000000000000, 0.000000000000000000, 0.000000000000000000 ) ) ;
#12269=ORIENTED_EDGE ( 'NONE', *, *, #3842, .T. ) ;
#12270=CARTESIAN_POINT ( 'NONE',  ( 31.00000000000001776, 0.000000000000000000, -25.99999999999999645 ) ) ;
#12277=FACE_OUTER_BOUND ( 'NONE', #13591, .T. ) ;
#12295=VERTEX_POINT ( 'NONE', #6949 ) ;
#12308=DIRECTION ( 'NONE',  ( 0.000000000000000000, 0.000000000000000000, -1.000000000000000000 ) ) ;
#12323=CARTESIAN_POINT ( 'NONE',  ( -26.00000000000002132, 8.000000000000000000, 40.00000000000000711 ) ) ;
#12330=FACE_BOUND ( 'NONE', #5408, .T. ) ;
#12351=CARTESIAN_POINT ( 'NONE',  ( -37.00000000000000711, 0.000000000000000000, 23.00000000000000000 ) ) ;
#12354=LINE ( 'NONE', #514, #969 ) ;
#12357=FACE_OUTER_BOUND ( 'NONE', #10051, .T. ) ;
#12360=AXIS2_PLACEMENT_3D ( 'NONE', #10567, #14348, #3870 ) ;
#12363=EDGE_CURVE ( 'NONE', #6935, #14554, #4802, .T. ) ;
#12365=CARTESIAN_POINT ( 'NONE',  ( 22.99999999999998224, 0.000000000000000000, -31.00000000000003197 ) ) ;
#12376=EDGE_LOOP ( 'NONE', ( #12504, #5785, #3485, #10907 ) ) ;
#12383=CARTESIAN_POINT ( 'NONE',  ( -23.00000000000002132, 10.00000000000000000, 37.00000000000000711 ) ) ;
#12391=ORIENTED_EDGE ( 'NONE', *, *, #15506, .F. ) ;
#12392=ORIENTED_EDGE ( 'NONE', *, *, #11141, .T. ) ;
#12393=VECTOR ( 'NONE', #9741, 1000.000000000000000 ) ;
#12396=ADVANCED_FACE ( 'NONE', ( #1889 ), #9963, .F. ) ;
#12407=CARTESIAN_POINT ( 'NONE',  ( 30.99999999999997868, 0.000000000000000000, -30.99999999999999645 ) ) ;
#12417=ORIENTED_EDGE ( 'NONE', *, *, #501, .F. ) ;
#12428=AXIS2_PLACEMENT_3D ( 'NONE', #5772, #5509, #14720 ) ;
#12434=ADVANCED_FACE ( 'NONE', ( #2135 ), #1969, .T. ) ;
#12439=DIRECTION ( 'NONE',  ( 1.000000000000000000, 0.000000000000000000, 0.000000000000000000 ) ) ;
#12446=ORIENTED_EDGE ( 'NONE', *, *, #1654, .T. ) ;
#12447=EDGE_CURVE ( 'NONE', #2065, #11864, #15203, .T. ) ;
#12458=AXIS2_PLACEMENT_3D ( 'NONE', #7695, #15364, #14249 ) ;
#12480=ADVANCED_FACE ( 'NONE', ( #2390 ), #10301, .T. ) ;
#12498=DIRECTION ( 'NONE',  ( -4.956352788505164254E-16, 0.000000000000000000, -1.000000000000000000 ) ) ;
#12504=ORIENTED_EDGE ( 'NONE', *, *, #6312, .F. ) ;
#12519=DIRECTION ( 'NONE',  ( -0.000000000000000000, -1.000000000000000000, -0.000000000000000000 ) ) ;
#12545=EDGE_CURVE ( 'NONE', #1812, #10736, #5867, .T. ) ;
#12557=CARTESIAN_POINT ( 'NONE',  ( 17.99999999999998224, 10.00000000000000000, -35.99999999999999289 ) ) ;
#12558=CARTESIAN_POINT ( 'NONE',  ( 35.99999999999999289, 8.000000000000000000, 18.99999999999999289 ) ) ;
#12564=EDGE_LOOP ( 'NONE', ( #5774, #5945, #12182, #12639 ) ) ;
#12575=DIRECTION ( 'NONE',  ( 0.000000000000000000, 0.000000000000000000, -1.000000000000000000 ) ) ;
#12577=FACE_OUTER_BOUND ( 'NONE', #1131, .T. ) ;
#12587=CARTESIAN_POINT ( 'NONE',  ( -19.00000000000001776, 10.00000000000000000, 40.00000000000000711 ) ) ;
#12595=ORIENTED_EDGE ( 'NONE', *, *, #12028, .F. ) ;
#12600=EDGE_CURVE ( 'NONE', #5055, #2354, #9184, .T. ) ;
#12608=VECTOR ( 'NONE', #14234, 1000.000000000000000 ) ;
#12614=DIRECTION ( 'NONE',  ( -0.000000000000000000, -0.000000000000000000, 1.000000000000000000 ) ) ;
#12621=DIRECTION ( 'NONE',  ( 0.000000000000000000, 0.000000000000000000, -1.000000000000000000 ) ) ;
#12626=CARTESIAN_POINT ( 'NONE',  ( 32.99999999999998579, 10.00000000000000000, 25.99999999999999645 ) ) ;
#12634=EDGE_CURVE ( 'NONE', #15298, #5706, #12187, .T. ) ;
#12639=ORIENTED_EDGE ( 'NONE', *, *, #8582, .T. ) ;
#12642=ORIENTED_EDGE ( 'NONE', *, *, #5354, .F. ) ;
#12657=DIRECTION ( 'NONE',  ( -0.000000000000000000, 1.000000000000000000, -0.000000000000000000 ) ) ;
#12663=PLANE ( 'NONE',  #11050 ) ;
#12668=( GEOMETRIC_REPRESENTATION_CONTEXT ( 3 ) GLOBAL_UNCERTAINTY_ASSIGNED_CONTEXT ( ( #13232 ) ) GLOBAL_UNIT_ASSIGNED_CONTEXT ( ( #11724, #10183, #16782 ) ) REPRESENTATION_CONTEXT ( 'NONE', 'WORKASPACE' ) );
#12671=ORIENTED_EDGE ( 'NONE', *, *, #7724, .T. ) ;
#12673=ORIENTED_EDGE ( 'NONE', *, *, #11590, .F. ) ;
#12680=VECTOR ( 'NONE', #12069, 1000.000000000000000 ) ;
#12684=CARTESIAN_POINT ( 'NONE',  ( -23.00000000000002132, 10.00000000000000000, 37.00000000000000711 ) ) ;
#12690=DIRECTION ( 'NONE',  ( -1.000000000000000000, -0.000000000000000000, 3.854941057726247958E-16 ) ) ;
#12695=DIRECTION ( 'NONE',  ( 0.000000000000000000, 1.000000000000000000, 0.000000000000000000 ) ) ;
#12729=ORIENTED_EDGE ( 'NONE', *, *, #1526, .T. ) ;
#12735=VECTOR ( 'NONE', #10753, 1000.000000000000000 ) ;
#12754=LINE ( 'NONE', #15653, #11325 ) ;
#12759=LINE ( 'NONE', #7587, #15521 ) ;
#12766=LINE ( 'NONE', #5180, #9139 ) ;
#12774=ORIENTED_EDGE ( 'NONE', *, *, #3295, .T. ) ;
#12776=VECTOR ( 'NONE', #2207, 1000.000000000000000 ) ;
#12791=ORIENTED_EDGE ( 'NONE', *, *, #6753, .T. ) ;
#12793=LINE ( 'NONE', #10302, #15860 ) ;
#12794=DIRECTION ( 'NONE',  ( 0.000000000000000000, 0.000000000000000000, 1.000000000000000000 ) ) ;
#12797=VECTOR ( 'NONE', #8141, 1000.000000000000000 ) ;
#12804=ADVANCED_FACE ( 'NONE', ( #16547 ), #15180, .T. ) ;
#12823=ORIENTED_EDGE ( 'NONE', *, *, #3109, .F. ) ;
#12825=DIRECTION ( 'NONE',  ( 1.000000000000000000, 0.000000000000000000, 0.000000000000000000 ) ) ;
#12834=LINE ( 'NONE', #3812, #484 ) ;
#12870=FACE_OUTER_BOUND ( 'NONE', #5356, .T. ) ;
#12878=EDGE_CURVE ( 'NONE', #10947, #13251, #2446, .T. ) ;
#12886=CARTESIAN_POINT ( 'NONE',  ( 17.99999999999998579, 6.000000000000000000, -36.99999999999999289 ) ) ;
#12900=ORIENTED_EDGE ( 'NONE', *, *, #8752, .F. ) ;
#12913=AXIS2_PLACEMENT_3D ( 'NONE', #9428, #3070, #13558 ) ;
#12917=CARTESIAN_POINT ( 'NONE',  ( 17.99999999999998224, 6.000000000000000000, -35.99999999999999289 ) ) ;
#12923=CARTESIAN_POINT ( 'NONE',  ( -22.00000000000001776, 8.000000000000000000, 33.00000000000000711 ) ) ;
#12942=ADVANCED_FACE ( 'NONE', ( #9069 ), #16957, .T. ) ;
#12943=VECTOR ( 'NONE', #6932, 1000.000000000000000 ) ;
#12967=DIRECTION ( 'NONE',  ( 1.000000000000000000, -0.000000000000000000, 0.000000000000000000 ) ) ;
#12968=ORIENTED_EDGE ( 'NONE', *, *, #829, .F. ) ;
#12971=AXIS2_PLACEMENT_3D ( 'NONE', #12923, #6380, #16872 ) ;
#12975=ADVANCED_FACE ( 'NONE', ( #2200 ), #1167, .T. ) ;
#12979=CARTESIAN_POINT ( 'NONE',  ( -37.00000000000000711, 6.000000000000000000, -18.00000000000000355 ) ) ;
#13002=ADVANCED_FACE ( 'NONE', ( #11647 ), #4864, .F. ) ;
#13010=ORIENTED_EDGE ( 'NONE', *, *, #3295, .F. ) ;
#13017=EDGE_CURVE ( 'NONE', #8178, #16566, #8912, .T. ) ;
#13021=DIRECTION ( 'NONE',  ( 0.000000000000000000, 1.000000000000000000, 0.000000000000000000 ) ) ;
#13028=DIRECTION ( 'NONE',  ( -0.000000000000000000, -1.000000000000000000, -0.000000000000000000 ) ) ;
#13032=CARTESIAN_POINT ( 'NONE',  ( 31.00000000000001421, 0.000000000000000000, 22.99999999999999645 ) ) ;
#13040=CARTESIAN_POINT ( 'NONE',  ( -33.00000000000000000, 8.000000000000000000, -26.00000000000000355 ) ) ;
#13045=DIRECTION ( 'NONE',  ( -1.000000000000000000, 0.000000000000000000, -0.000000000000000000 ) ) ;
#13067=AXIS2_PLACEMENT_3D ( 'NONE', #6166, #780, #7114 ) ;
#13079=ORIENTED_EDGE ( 'NONE', *, *, #14643, .T. ) ;
#13099=EDGE_CURVE ( 'NONE', #971, #4249, #13288, .T. ) ;
#13106=DIRECTION ( 'NONE',  ( 0.000000000000000000, 0.000000000000000000, 1.000000000000000000 ) ) ;
#13108=FACE_OUTER_BOUND ( 'NONE', #9041, .T. ) ;
#13124=FACE_OUTER_BOUND ( 'NONE', #3802, .T. ) ;
#13148=DIRECTION ( 'NONE',  ( 0.000000000000000000, 1.000000000000000000, 0.000000000000000000 ) ) ;
#13169=CARTESIAN_POINT ( 'NONE',  ( -22.00000000000001776, 8.000000000000000000, 36.00000000000000711 ) ) ;
#13171=CARTESIAN_POINT ( 'NONE',  ( -37.00000000000000711, 10.00000000000000000, 23.00000000000000000 ) ) ;
#13177=CARTESIAN_POINT ( 'NONE',  ( 21.99999999999998224, 10.00000000000000000, -32.99999999999999289 ) ) ;
#13180=FACE_OUTER_BOUND ( 'NONE', #8640, .T. ) ;
#13187=EDGE_CURVE ( 'NONE', #7379, #594, #8203, .T. ) ;
#13188=AXIS2_PLACEMENT_3D ( 'NONE', #8843, #1194, #6411 ) ;
#13192=DIRECTION ( 'NONE',  ( 0.000000000000000000, 1.000000000000000000, 0.000000000000000000 ) ) ;
#13206=VECTOR ( 'NONE', #16602, 1000.000000000000000 ) ;
#13232=UNCERTAINTY_MEASURE_WITH_UNIT (LENGTH_MEASURE( 1.000000000000000082E-05 ), #11724, 'distance_accuracy_value', 'NONE');
#13234=CARTESIAN_POINT ( 'NONE',  ( -23.00000000000002487, 10.00000000000000000, -31.00000000000003553 ) ) ;
#13239=DIRECTION ( 'NONE',  ( 1.000000000000000000, 0.000000000000000000, 0.000000000000000000 ) ) ;
#13240=ORIENTED_EDGE ( 'NONE', *, *, #5204, .T. ) ;
#13251=VERTEX_POINT ( 'NONE', #3307 ) ;
#13258=LINE ( 'NONE', #16763, #15177 ) ;
#13261=AXIS2_PLACEMENT_3D ( 'NONE', #7510, #9544, #5978 ) ;
#13276=ADVANCED_FACE ( 'NONE', ( #4594 ), #5713, .F. ) ;
#13280=VECTOR ( 'NONE', #7934, 1000.000000000000000 ) ;
#13282=LINE ( 'NONE', #227, #8885 ) ;
#13285=AXIS2_PLACEMENT_3D ( 'NONE', #8822, #5029, #1172 ) ;
#13288=LINE ( 'NONE', #10876, #9864 ) ;
#13290=CARTESIAN_POINT ( 'NONE',  ( 22.99999999999998224, 10.00000000000000000, -31.99999999999998579 ) ) ;
#13311=ORIENTED_EDGE ( 'NONE', *, *, #5311, .T. ) ;
#13319=ORIENTED_EDGE ( 'NONE', *, *, #9472, .F. ) ;
#13343=ORIENTED_EDGE ( 'NONE', *, *, #9601, .F. ) ;
#13349=ORIENTED_EDGE ( 'NONE', *, *, #7804, .T. ) ;
#13352=ORIENTED_EDGE ( 'NONE', *, *, #8448, .T. ) ;
#13353=FACE_OUTER_BOUND ( 'NONE', #14956, .T. ) ;
#13359=VECTOR ( 'NONE', #12308, 1000.000000000000000 ) ;
#13362=DIRECTION ( 'NONE',  ( 0.000000000000000000, 0.000000000000000000, -1.000000000000000000 ) ) ;
#13388=ADVANCED_FACE ( 'NONE', ( #15497 ), #14207, .F. ) ;
#13398=EDGE_CURVE ( 'NONE', #3717, #2065, #16767, .T. ) ;
#13401=ADVANCED_FACE ( 'NONE', ( #10008 ), #15243, .T. ) ;
#13403=CARTESIAN_POINT ( 'NONE',  ( -18.00000000000001421, 10.00000000000000000, 37.00000000000000711 ) ) ;
#13411=EDGE_CURVE ( 'NONE', #10297, #3745, #11371, .T. ) ;
#13419=CARTESIAN_POINT ( 'NONE',  ( 21.99999999999998224, 6.000000000000000000, -35.99999999999999289 ) ) ;
#13454=DIRECTION ( 'NONE',  ( -0.000000000000000000, -1.000000000000000000, 0.000000000000000000 ) ) ;
#13455=PRODUCT ( 'Servo-Body.2', 'Servo-Body.2', '', ( #13752 ) ) ;
#13464=LINE ( 'NONE', #13709, #933 ) ;
#13465=DIRECTION ( 'NONE',  ( 1.000000000000000000, 0.000000000000000000, 0.000000000000000000 ) ) ;
#13482=CARTESIAN_POINT ( 'NONE',  ( 39.99999999999999289, 0.000000000000000000, 26.00000000000000000 ) ) ;
#13507=VERTEX_POINT ( 'NONE', #11010 ) ;
#13528=AXIS2_PLACEMENT_3D ( 'NONE', #3432, #7437, #7278 ) ;
#13529=EDGE_LOOP ( 'NONE', ( #11455, #16511, #10047, #9497, #7492, #6714 ) ) ;
#13547=DIRECTION ( 'NONE',  ( -0.000000000000000000, -1.000000000000000000, -0.000000000000000000 ) ) ;
#13558=DIRECTION ( 'NONE',  ( 1.000000000000000000, 0.000000000000000000, -3.854941057726258312E-16 ) ) ;
#13563=( GEOMETRIC_REPRESENTATION_CONTEXT ( 3 ) GLOBAL_UNCERTAINTY_ASSIGNED_CONTEXT ( ( #14600 ) ) GLOBAL_UNIT_ASSIGNED_CONTEXT ( ( #955, #16583, #3612 ) ) REPRESENTATION_CONTEXT ( 'NONE', 'WORKASPACE' ) );
#13569=CARTESIAN_POINT ( 'NONE',  ( 25.99999999999997868, 10.00000000000000000, -39.99999999999999289 ) ) ;
#13575=CARTESIAN_POINT ( 'NONE',  ( -22.00000000000001776, 8.000000000000000000, 36.00000000000000711 ) ) ;
#13591=EDGE_LOOP ( 'NONE', ( #908, #11899, #6682, #9035 ) ) ;
#13608=CARTESIAN_POINT ( 'NONE',  ( -18.00000000000001421, 6.000000000000000000, 40.00000000000000711 ) ) ;
#13609=ORIENTED_EDGE ( 'NONE', *, *, #143, .F. ) ;
#13629=CARTESIAN_POINT ( 'NONE',  ( 35.99999999999999289, 6.000000000000000000, 21.99999999999999645 ) ) ;
#13657=LINE ( 'NONE', #7434, #9872 ) ;
#13669=ADVANCED_FACE ( 'NONE', ( #7969 ), #4385, .F. ) ;
#13693=VERTEX_POINT ( 'NONE', #2920 ) ;
#13709=CARTESIAN_POINT ( 'NONE',  ( 36.99999999999999289, 6.000000000000000000, 22.99999999999999645 ) ) ;
#13715=EDGE_CURVE ( 'NONE', #15604, #4249, #935, .T. ) ;
#13718=EDGE_CURVE ( 'NONE', #3738, #1429, #13657, .T. ) ;
#13723=EDGE_CURVE ( 'NONE', #2662, #1311, #5176, .T. ) ;
#13724=VECTOR ( 'NONE', #9773, 1000.000000000000000 ) ;
#13748=ORIENTED_EDGE ( 'NONE', *, *, #8020, .T. ) ;
#13752=PRODUCT_CONTEXT ( 'NONE', #306, 'mechanical' ) ;
#13755=ORIENTED_EDGE ( 'NONE', *, *, #8559, .F. ) ;
#13759=DIRECTION ( 'NONE',  ( 1.156482317317881191E-15, 0.000000000000000000, 1.000000000000000000 ) ) ;
#13764=ORIENTED_EDGE ( 'NONE', *, *, #13017, .F. ) ;
#13765=ORIENTED_EDGE ( 'NONE', *, *, #11970, .T. ) ;
#13770=VECTOR ( 'NONE', #3588, 1000.000000000000000 ) ;
#13774=CARTESIAN_POINT ( 'NONE',  ( -31.00000000000005329, 0.000000000000000000, 26.00000000000000000 ) ) ;
#13781=DIRECTION ( 'NONE',  ( 1.000000000000000000, 0.000000000000000000, 3.854941057726246479E-16 ) ) ;
#13786=CARTESIAN_POINT ( 'NONE',  ( 31.99999999999998579, 10.00000000000000000, 22.99999999999999645 ) ) ;
#13787=DIRECTION ( 'NONE',  ( 0.000000000000000000, 1.000000000000000000, 0.000000000000000000 ) ) ;
#13793=EDGE_CURVE ( 'NONE', #6668, #221, #7273, .T. ) ;
#13802=VECTOR ( 'NONE', #15324, 1000.000000000000000 ) ;
#13810=VECTOR ( 'NONE', #5879, 1000.000000000000000 ) ;
#13811=DIRECTION ( 'NONE',  ( -0.000000000000000000, 1.000000000000000000, -0.000000000000000000 ) ) ;
#13823=CARTESIAN_POINT ( 'NONE',  ( 30.99999999999997513, 0.000000000000000000, 30.99999999999999645 ) ) ;
#13830=CARTESIAN_POINT ( 'NONE',  ( -23.00000000000002487, 0.000000000000000000, -31.00000000000003553 ) ) ;
#13858=ORIENTED_EDGE ( 'NONE', *, *, #10805, .F. ) ;
#13867=CARTESIAN_POINT ( 'NONE',  ( 18.99999999999998224, 8.000000000000000000, -39.99999999999999289 ) ) ;
#13873=DIRECTION ( 'NONE',  ( 0.000000000000000000, 0.000000000000000000, -1.000000000000000000 ) ) ;
#13877=ORIENTED_EDGE ( 'NONE', *, *, #11970, .F. ) ;
#13880=ORIENTED_EDGE ( 'NONE', *, *, #15800, .T. ) ;
#13887=VECTOR ( 'NONE', #15028, 1000.000000000000000 ) ;
#13905=ADVANCED_FACE ( 'NONE', ( #68 ), #10118, .F. ) ;
#13906=DIRECTION ( 'NONE',  ( -0.000000000000000000, -1.000000000000000000, -0.000000000000000000 ) ) ;
#13914=VECTOR ( 'NONE', #15128, 1000.000000000000000 ) ;
#13930=DIRECTION ( 'NONE',  ( -3.854941057726253874E-16, 0.000000000000000000, -1.000000000000000000 ) ) ;
#13935=ORIENTED_EDGE ( 'NONE', *, *, #1106, .F. ) ;
#13946=PRODUCT_DEFINITION_CONTEXT ( 'detailed design', #76, 'design' ) ;
#13952=DIRECTION ( 'NONE',  ( 0.000000000000000000, 0.000000000000000000, -1.000000000000000000 ) ) ;
#13956=DIRECTION ( 'NONE',  ( 1.000000000000000000, -0.000000000000000000, 0.000000000000000000 ) ) ;
#13980=DIRECTION ( 'NONE',  ( -1.000000000000000000, -0.000000000000000000, -8.673617379884027583E-16 ) ) ;
#13983=EDGE_CURVE ( 'NONE', #1948, #1911, #1527, .T. ) ;
#13984=DIRECTION ( 'NONE',  ( 1.000000000000000000, 0.000000000000000000, 0.000000000000000000 ) ) ;
#13985=DIRECTION ( 'NONE',  ( -0.000000000000000000, -1.000000000000000000, 0.000000000000000000 ) ) ;
#13992=DIRECTION ( 'NONE',  ( 0.000000000000000000, 0.000000000000000000, -1.000000000000000000 ) ) ;
#13994=CARTESIAN_POINT ( 'NONE',  ( -26.00000000000001776, 10.00000000000000000, 33.00000000000000711 ) ) ;
#13995=CARTESIAN_POINT ( 'NONE',  ( -36.00000000000000711, 8.000000000000000000, -19.00000000000000000 ) ) ;
#14001=ORIENTED_EDGE ( 'NONE', *, *, #5398, .F. ) ;
#14016=VERTEX_POINT ( 'NONE', #579 ) ;
#14020=ORIENTED_EDGE ( 'NONE', *, *, #3913, .T. ) ;
#14044=VERTEX_POINT ( 'NONE', #16533 ) ;
#14055=DIRECTION ( 'NONE',  ( 1.000000000000000000, -0.000000000000000000, 4.956352788505159323E-16 ) ) ;
#14057=ORIENTED_EDGE ( 'NONE', *, *, #11492, .T. ) ;
#14071=CARTESIAN_POINT ( 'NONE',  ( -26.00000000000002132, 10.00000000000000000, -39.99999999999999289 ) ) ;
#14072=CIRCLE ( 'NONE', #13261, 2.999999999999995559 ) ;
#14073=FACE_OUTER_BOUND ( 'NONE', #16769, .T. ) ;
#14076=CIRCLE ( 'NONE', #6657, 4.999999999999997335 ) ;
#14085=ORIENTED_EDGE ( 'NONE', *, *, #15292, .T. ) ;
#14092=ORIENTED_EDGE ( 'NONE', *, *, #5935, .T. ) ;
#14109=CARTESIAN_POINT ( 'NONE',  ( -26.00000000000001776, 8.000000000000000000, 33.00000000000000711 ) ) ;
#14110=VECTOR ( 'NONE', #6087, 1000.000000000000000 ) ;
#14111=MANIFOLD_SOLID_BREP ( 'Cut-Extrude1', #4968 ) ;
#14112=ORIENTED_EDGE ( 'NONE', *, *, #3264, .F. ) ;
#14125=VECTOR ( 'NONE', #16135, 1000.000000000000000 ) ;
#14127=ADVANCED_FACE ( 'NONE', ( #2620 ), #14221, .T. ) ;
#14131=CARTESIAN_POINT ( 'NONE',  ( -31.00000000000001776, 10.00000000000000000, 31.00000000000000000 ) ) ;
#14137=VERTEX_POINT ( 'NONE', #2358 ) ;
#14150=CARTESIAN_POINT ( 'NONE',  ( -37.00000000000000711, 0.000000000000000000, 23.00000000000000000 ) ) ;
#14154=LINE ( 'NONE', #2537, #1434 ) ;
#14155=DIRECTION ( 'NONE',  ( 0.000000000000000000, 0.000000000000000000, -1.000000000000000000 ) ) ;
#14161=AXIS2_PLACEMENT_3D ( 'NONE', #9435, #11925, #9604 ) ;
#14163=ORIENTED_EDGE ( 'NONE', *, *, #7997, .F. ) ;
#14170=LINE ( 'NONE', #1192, #15259 ) ;
#14183=DIRECTION ( 'NONE',  ( 1.000000000000000000, 0.000000000000000000, 0.000000000000000000 ) ) ;
#14199=ADVANCED_FACE ( 'NONE', ( #4083 ), #1508, .T. ) ;
#14205=LINE ( 'NONE', #16931, #1745 ) ;
#14207=PLANE ( 'NONE',  #6574 ) ;
#14211=CARTESIAN_POINT ( 'NONE',  ( 25.99999999999997513, 10.00000000000000000, 31.00000000000003553 ) ) ;
#14220=EDGE_LOOP ( 'NONE', ( #8874, #10794, #8703, #15260, #3033, #5175 ) ) ;
#14221=PLANE ( 'NONE',  #1984 ) ;
#14226=EDGE_LOOP ( 'NONE', ( #14611, #2762, #6286, #7749, #10010, #3214 ) ) ;
#14227=DIRECTION ( 'NONE',  ( 0.000000000000000000, 0.000000000000000000, -1.000000000000000000 ) ) ;
#14231=EDGE_CURVE ( 'NONE', #9832, #4632, #12157, .T. ) ;
#14234=DIRECTION ( 'NONE',  ( 1.000000000000000000, 0.000000000000000000, 0.000000000000000000 ) ) ;
#14238=ADVANCED_FACE ( 'NONE', ( #14560 ), #2783, .F. ) ;
#14243=CARTESIAN_POINT ( 'NONE',  ( 22.99999999999998224, 10.00000000000000000, -31.00000000000003197 ) ) ;
#14245=DIRECTION ( 'NONE',  ( 0.000000000000000000, 0.000000000000000000, 1.000000000000000000 ) ) ;
#14249=DIRECTION ( 'NONE',  ( 0.000000000000000000, 0.000000000000000000, 1.000000000000000000 ) ) ;
#14282=VERTEX_POINT ( 'NONE', #13774 ) ;
#14297=FACE_OUTER_BOUND ( 'NONE', #14818, .T. ) ;
#14303=CARTESIAN_POINT ( 'NONE',  ( -33.00000000000000000, 8.000000000000000000, -22.00000000000000355 ) ) ;
#14310=CARTESIAN_POINT ( 'NONE',  ( 21.99999999999998224, 6.000000000000000000, -31.99999999999998579 ) ) ;
#14311=LINE ( 'NONE', #9253, #146 ) ;
#14314=AXIS2_PLACEMENT_3D ( 'NONE', #5422, #5599, #205 ) ;
#14322=EDGE_CURVE ( 'NONE', #12051, #2662, #2002, .T. ) ;
#14323=DIRECTION ( 'NONE',  ( 0.000000000000000000, 0.000000000000000000, 1.000000000000000000 ) ) ;
#14325=PLANE ( 'NONE',  #16080 ) ;
#14348=DIRECTION ( 'NONE',  ( 1.000000000000000000, -0.000000000000000000, 0.000000000000000000 ) ) ;
#14369=CARTESIAN_POINT ( 'NONE',  ( 35.99999999999999289, 10.00000000000000000, 17.99999999999998934 ) ) ;
#14375=DIRECTION ( 'NONE',  ( 0.000000000000000000, 0.000000000000000000, -1.000000000000000000 ) ) ;
#14381=VECTOR ( 'NONE', #12614, 1000.000000000000000 ) ;
#14390=SURFACE_SIDE_STYLE ('',( #6465 ) ) ;
#14393=CARTESIAN_POINT ( 'NONE',  ( 31.00000000000003553, 10.00000000000000000, -22.99999999999999645 ) ) ;
#14399=DIRECTION ( 'NONE',  ( -0.000000000000000000, -0.000000000000000000, 1.000000000000000000 ) ) ;
#14405=ORIENTED_EDGE ( 'NONE', *, *, #16352, .F. ) ;
#14406=ORIENTED_EDGE ( 'NONE', *, *, #10615, .F. ) ;
#14410=FACE_OUTER_BOUND ( 'NONE', #3360, .T. ) ;
#14412=EDGE_CURVE ( 'NONE', #10374, #10263, #5399, .T. ) ;
#14416=DIRECTION ( 'NONE',  ( 0.000000000000000000, 0.000000000000000000, 1.000000000000000000 ) ) ;
#14427=ADVANCED_FACE ( 'NONE', ( #14512 ), #15710, .F. ) ;
#14441=VECTOR ( 'NONE', #10209, 1000.000000000000000 ) ;
#14444=DIRECTION ( 'NONE',  ( 0.000000000000000000, 0.000000000000000000, 1.000000000000000000 ) ) ;
#14451=ORIENTED_EDGE ( 'NONE', *, *, #6753, .F. ) ;
#14468=ORIENTED_EDGE ( 'NONE', *, *, #14545, .F. ) ;
#14479=EDGE_CURVE ( 'NONE', #4138, #9177, #6111, .T. ) ;
#14491=DIRECTION ( 'NONE',  ( 0.000000000000000000, -1.000000000000000000, 0.000000000000000000 ) ) ;
#14499=PLANE ( 'NONE',  #8027 ) ;
#14502=CARTESIAN_POINT ( 'NONE',  ( 30.99999999999997513, 10.00000000000000000, 30.99999999999999645 ) ) ;
#14512=FACE_OUTER_BOUND ( 'NONE', #2934, .T. ) ;
#14528=LINE ( 'NONE', #5417, #11095 ) ;
#14536=VECTOR ( 'NONE', #13465, 1000.000000000000000 ) ;
#14540=LINE ( 'NONE', #10591, #1182 ) ;
#14542=VERTEX_POINT ( 'NONE', #14857 ) ;
#14545=EDGE_CURVE ( 'NONE', #12295, #4162, #345, .T. ) ;
#14552=EDGE_CURVE ( 'NONE', #11763, #3738, #8326, .T. ) ;
#14554=VERTEX_POINT ( 'NONE', #10823 ) ;
#14558=ORIENTED_EDGE ( 'NONE', *, *, #8643, .T. ) ;
#14560=FACE_OUTER_BOUND ( 'NONE', #10835, .T. ) ;
#14564=CARTESIAN_POINT ( 'NONE',  ( 36.99999999999999289, 0.000000000000000000, 22.99999999999999645 ) ) ;
#14571=EDGE_CURVE ( 'NONE', #2235, #4006, #11159, .T. ) ;
#14573=EDGE_LOOP ( 'NONE', ( #5988, #8229, #7538, #3908 ) ) ;
#14581=VECTOR ( 'NONE', #764, 1000.000000000000000 ) ;
#14585=VERTEX_POINT ( 'NONE', #15356 ) ;
#14597=DIRECTION ( 'NONE',  ( 0.000000000000000000, 0.000000000000000000, -1.000000000000000000 ) ) ;
#14600=UNCERTAINTY_MEASURE_WITH_UNIT (LENGTH_MEASURE( 1.000000000000000082E-05 ), #955, 'distance_accuracy_value', 'NONE');
#14605=VECTOR ( 'NONE', #5093, 1000.000000000000000 ) ;
#14606=VECTOR ( 'NONE', #14597, 1000.000000000000000 ) ;
#14611=ORIENTED_EDGE ( 'NONE', *, *, #5075, .F. ) ;
#14616=ADVANCED_FACE ( 'NONE', ( #8751 ), #11072, .F. ) ;
#14636=CARTESIAN_POINT ( 'NONE',  ( 32.99999999999998579, 10.00000000000000000, 21.99999999999999645 ) ) ;
#14643=EDGE_CURVE ( 'NONE', #11379, #7379, #6641, .T. ) ;
#14644=EDGE_CURVE ( 'NONE', #2707, #15120, #4623, .T. ) ;
#14649=DIRECTION ( 'NONE',  ( 1.000000000000000000, 0.000000000000000000, -0.000000000000000000 ) ) ;
#14657=ADVANCED_FACE ( 'NONE', ( #10043 ), #9871, .F. ) ;
#14667=VECTOR ( 'NONE', #9385, 1000.000000000000000 ) ;
#14668=LINE ( 'NONE', #4359, #11784 ) ;
#14675=DIRECTION ( 'NONE',  ( 1.000000000000000000, 0.000000000000000000, -3.854941057726247958E-16 ) ) ;
#14698=ORIENTED_EDGE ( 'NONE', *, *, #10570, .F. ) ;
#14706=EDGE_LOOP ( 'NONE', ( #4073, #9897, #14001, #8139 ) ) ;
#14709=ORIENTED_EDGE ( 'NONE', *, *, #16630, .T. ) ;
#14720=DIRECTION ( 'NONE',  ( 0.000000000000000000, 0.000000000000000000, -1.000000000000000000 ) ) ;
#14730=VECTOR ( 'NONE', #16458, 1000.000000000000000 ) ;
#14732=ORIENTED_EDGE ( 'NONE', *, *, #3236, .T. ) ;
#14733=EDGE_CURVE ( 'NONE', #9305, #9092, #15440, .T. ) ;
#14738=CARTESIAN_POINT ( 'NONE',  ( -18.00000000000001421, 6.000000000000000000, 36.00000000000000711 ) ) ;
#14752=VERTEX_POINT ( 'NONE', #3683 ) ;
#14762=VECTOR ( 'NONE', #11230, 1000.000000000000000 ) ;
#14763=DIRECTION ( 'NONE',  ( 0.000000000000000000, 0.000000000000000000, -1.000000000000000000 ) ) ;
#14765=ADVANCED_FACE ( 'NONE', ( #13124 ), #14499, .F. ) ;
#14767=DIRECTION ( 'NONE',  ( 1.000000000000000000, 0.000000000000000000, 0.000000000000000000 ) ) ;
#14788=CARTESIAN_POINT ( 'NONE',  ( -31.00000000000001776, 0.000000000000000000, 31.00000000000000000 ) ) ;
#14789=DIRECTION ( 'NONE',  ( 0.000000000000000000, 0.000000000000000000, -1.000000000000000000 ) ) ;
#14818=EDGE_LOOP ( 'NONE', ( #16626, #6652, #13765, #8867, #14092 ) ) ;
#14821=LINE ( 'NONE', #4263, #3132 ) ;
#14833=VERTEX_POINT ( 'NONE', #2637 ) ;
#14838=PLANE ( 'NONE',  #12913 ) ;
#14843=ADVANCED_FACE ( 'NONE', ( #11566 ), #16800, .T. ) ;
#14857=CARTESIAN_POINT ( 'NONE',  ( 39.99999999999999289, 10.00000000000000000, 18.99999999999999645 ) ) ;
#14859=LINE ( 'NONE', #6589, #11310 ) ;
#14861=EDGE_CURVE ( 'NONE', #777, #15604, #11326, .T. ) ;
#14870=EDGE_LOOP ( 'NONE', ( #238, #5193, #6789, #329 ) ) ;
#14871=ORIENTED_EDGE ( 'NONE', *, *, #6011, .T. ) ;
#14876=ORIENTED_EDGE ( 'NONE', *, *, #8662, .F. ) ;
#14882=ORIENTED_EDGE ( 'NONE', *, *, #12634, .F. ) ;
#14886=ORIENTED_EDGE ( 'NONE', *, *, #13715, .F. ) ;
#14887=VECTOR ( 'NONE', #1272, 1000.000000000000000 ) ;
#14895=ORIENTED_EDGE ( 'NONE', *, *, #9413, .F. ) ;
#14898=VECTOR ( 'NONE', #10339, 1000.000000000000000 ) ;
#14918=LINE ( 'NONE', #5723, #3716 ) ;
#14921=EDGE_CURVE ( 'NONE', #9305, #6283, #14925, .T. ) ;
#14925=LINE ( 'NONE', #4101, #367 ) ;
#14927=ORIENTED_EDGE ( 'NONE', *, *, #13983, .F. ) ;
#14937=PRODUCT_DEFINITION ( 'UNKNOWN', '', #15223, #13946 ) ;
#14940=DIRECTION ( 'NONE',  ( 0.000000000000000000, 0.000000000000000000, -1.000000000000000000 ) ) ;
#14945=DIRECTION ( 'NONE',  ( -0.000000000000000000, 1.000000000000000000, -0.000000000000000000 ) ) ;
#14946=VECTOR ( 'NONE', #14055, 1000.000000000000000 ) ;
#14956=EDGE_LOOP ( 'NONE', ( #10079, #1828, #1493, #10515 ) ) ;
#14958=DIRECTION ( 'NONE',  ( 0.000000000000000000, 1.000000000000000000, 0.000000000000000000 ) ) ;
#14960=ORIENTED_EDGE ( 'NONE', *, *, #4384, .T. ) ;
#14965=ADVANCED_FACE ( 'NONE', ( #6666 ), #9429, .F. ) ;
#14970=CARTESIAN_POINT ( 'NONE',  ( 22.99999999999998224, 10.00000000000000000, -31.00000000000003197 ) ) ;
#14978=VERTEX_POINT ( 'NONE', #12088 ) ;
#14987=ORIENTED_EDGE ( 'NONE', *, *, #6342, .T. ) ;
#14988=VERTEX_POINT ( 'NONE', #6052 ) ;
#14993=CARTESIAN_POINT ( 'NONE',  ( 25.99999999999997868, 10.00000000000000000, 40.00000000000000711 ) ) ;
#15006=DIRECTION ( 'NONE',  ( -0.000000000000000000, -1.000000000000000000, -0.000000000000000000 ) ) ;
#15026=DIRECTION ( 'NONE',  ( -1.000000000000000000, -0.000000000000000000, 3.854941057726258312E-16 ) ) ;
#15028=DIRECTION ( 'NONE',  ( 0.000000000000000000, 1.000000000000000000, 0.000000000000000000 ) ) ;
#15041=ORIENTED_EDGE ( 'NONE', *, *, #15802, .T. ) ;
#15042=ADVANCED_FACE ( 'NONE', ( #667 ), #8651, .F. ) ;
#15048=LINE ( 'NONE', #799, #13914 ) ;
#15056=EDGE_LOOP ( 'NONE', ( #922, #7141, #10772, #6244, #730, #11157 ) ) ;
#15057=ORIENTED_EDGE ( 'NONE', *, *, #5308, .F. ) ;
#15082=CARTESIAN_POINT ( 'NONE',  ( 21.99999999999998224, 6.000000000000000000, -31.99999999999998579 ) ) ;
#15087=VECTOR ( 'NONE', #16368, 1000.000000000000000 ) ;
#15094=LINE ( 'NONE', #8574, #7708 ) ;
#15112=CARTESIAN_POINT ( 'NONE',  ( 35.99999999999999289, 6.000000000000000000, 21.99999999999999645 ) ) ;
#15120=VERTEX_POINT ( 'NONE', #2110 ) ;
#15128=DIRECTION ( 'NONE',  ( -0.000000000000000000, -1.000000000000000000, -0.000000000000000000 ) ) ;
#15134=EDGE_CURVE ( 'NONE', #5278, #16003, #12766, .T. ) ;
#15138=VECTOR ( 'NONE', #15674, 1000.000000000000000 ) ;
#15177=VECTOR ( 'NONE', #122, 1000.000000000000000 ) ;
#15180=PLANE ( 'NONE',  #9620 ) ;
#15184=VECTOR ( 'NONE', #12657, 1000.000000000000000 ) ;
#15197=CARTESIAN_POINT ( 'NONE',  ( -37.00000000000000711, 10.00000000000000000, 23.00000000000000000 ) ) ;
#15203=LINE ( 'NONE', #8677, #16572 ) ;
#15208=AXIS2_PLACEMENT_3D ( 'NONE', #15616, #15449, #6320 ) ;
#15217=DIRECTION ( 'NONE',  ( 1.000000000000000000, 0.000000000000000000, 0.000000000000000000 ) ) ;
#15220=VERTEX_POINT ( 'NONE', #10520 ) ;
#15223=PRODUCT_DEFINITION_FORMATION_WITH_SPECIFIED_SOURCE ( 'ANY', '', #13455, .NOT_KNOWN. ) ;
#15225=CARTESIAN_POINT ( 'NONE',  ( 30.99999999999997868, 0.000000000000000000, -30.99999999999999645 ) ) ;
#15227=ORIENTED_EDGE ( 'NONE', *, *, #16022, .F. ) ;
#15235=ORIENTED_EDGE ( 'NONE', *, *, #1106, .T. ) ;
#15239=DIRECTION ( 'NONE',  ( -0.000000000000000000, -1.000000000000000000, 0.000000000000000000 ) ) ;
#15243=PLANE ( 'NONE',  #5736 ) ;
#15246=DIRECTION ( 'NONE',  ( 0.000000000000000000, -1.000000000000000000, 0.000000000000000000 ) ) ;
#15259=VECTOR ( 'NONE', #5301, 1000.000000000000000 ) ;
#15260=ORIENTED_EDGE ( 'NONE', *, *, #8020, .F. ) ;
#15261=ADVANCED_FACE ( 'NONE', ( #13108 ), #2441, .F. ) ;
#15280=EDGE_CURVE ( 'NONE', #14137, #15298, #13282, .T. ) ;
#15290=VERTEX_POINT ( 'NONE', #4005 ) ;
#15292=EDGE_CURVE ( 'NONE', #5130, #8924, #14821, .T. ) ;
#15298=VERTEX_POINT ( 'NONE', #4349 ) ;
#15309=ORIENTED_EDGE ( 'NONE', *, *, #8448, .F. ) ;
#15318=ORIENTED_EDGE ( 'NONE', *, *, #3490, .F. ) ;
#15324=DIRECTION ( 'NONE',  ( 0.000000000000000000, 1.000000000000000000, 0.000000000000000000 ) ) ;
#15337=VECTOR ( 'NONE', #10090, 1000.000000000000000 ) ;
#15349=AXIS2_PLACEMENT_3D ( 'NONE', #4697, #12695, #4547 ) ;
#15350=FACE_OUTER_BOUND ( 'NONE', #3454, .T. ) ;
#15356=CARTESIAN_POINT ( 'NONE',  ( -32.00000000000000711, 10.00000000000000000, -23.00000000000000000 ) ) ;
#15358=CIRCLE ( 'NONE', #8220, 3.000000000000002665 ) ;
#15361=CARTESIAN_POINT ( 'NONE',  ( 21.99999999999998224, 8.000000000000000000, -35.99999999999999289 ) ) ;
#15363=ORIENTED_EDGE ( 'NONE', *, *, #16865, .F. ) ;
#15364=DIRECTION ( 'NONE',  ( 0.000000000000000000, 1.000000000000000000, 0.000000000000000000 ) ) ;
#15368=CARTESIAN_POINT ( 'NONE',  ( -33.00000000000000000, 10.00000000000000000, -22.00000000000000355 ) ) ;
#15377=EDGE_CURVE ( 'NONE', #11680, #13507, #8021, .T. ) ;
#15378=DIRECTION ( 'NONE',  ( -0.000000000000000000, -1.000000000000000000, -0.000000000000000000 ) ) ;
#15392=ORIENTED_EDGE ( 'NONE', *, *, #3946, .F. ) ;
#15400=CARTESIAN_POINT ( 'NONE',  ( 30.99999999999997513, 10.00000000000000000, 25.99999999999999645 ) ) ;
#15401=PLANE ( 'NONE',  #9834 ) ;
#15402=LINE ( 'NONE', #7483, #13802 ) ;
#15404=CIRCLE ( 'NONE', #14314, 3.999999999999996447 ) ;
#15409=DIRECTION ( 'NONE',  ( -0.000000000000000000, 0.000000000000000000, 1.000000000000000000 ) ) ;
#15418=DIRECTION ( 'NONE',  ( 1.000000000000000000, 0.000000000000000000, -0.000000000000000000 ) ) ;
#15425=CARTESIAN_POINT ( 'NONE',  ( -31.00000000000007105, 0.000000000000000000, 23.00000000000000000 ) ) ;
#15432=LINE ( 'NONE', #10291, #3960 ) ;
#15436=VECTOR ( 'NONE', #3156, 1000.000000000000000 ) ;
#15440=LINE ( 'NONE', #3769, #1165 ) ;
#15449=DIRECTION ( 'NONE',  ( 0.000000000000000000, 0.000000000000000000, 1.000000000000000000 ) ) ;
#15473=FACE_OUTER_BOUND ( 'NONE', #14870, .T. ) ;
#15475=VECTOR ( 'NONE', #2139, 1000.000000000000000 ) ;
#15476=CARTESIAN_POINT ( 'NONE',  ( -26.00000000000001776, 8.000000000000000000, 33.00000000000000711 ) ) ;
#15497=FACE_OUTER_BOUND ( 'NONE', #16930, .T. ) ;
#15499=EDGE_CURVE ( 'NONE', #6145, #2977, #2092, .T. ) ;
#15506=EDGE_CURVE ( 'NONE', #16566, #5055, #2560, .T. ) ;
#15520=DIRECTION ( 'NONE',  ( -0.000000000000000000, 1.000000000000000000, -0.000000000000000000 ) ) ;
#15521=VECTOR ( 'NONE', #2274, 1000.000000000000000 ) ;
#15523=CARTESIAN_POINT ( 'NONE',  ( -26.00000000000002132, 10.00000000000000000, -39.99999999999999289 ) ) ;
#15525=DIRECTION ( 'NONE',  ( -0.000000000000000000, -1.000000000000000000, -0.000000000000000000 ) ) ;
#15552=VERTEX_POINT ( 'NONE', #12323 ) ;
#15554=LINE ( 'NONE', #3867, #1156 ) ;
#15568=ORIENTED_EDGE ( 'NONE', *, *, #9413, .T. ) ;
#15574=ORIENTED_EDGE ( 'NONE', *, *, #14644, .F. ) ;
#15584=AXIS2_PLACEMENT_3D ( 'NONE', #13419, #13148, #356 ) ;
#15587=FILL_AREA_STYLE_COLOUR ( '', #11027 ) ;
#15593=ORIENTED_EDGE ( 'NONE', *, *, #5354, .T. ) ;
#15596=DIRECTION ( 'NONE',  ( 0.000000000000000000, -0.000000000000000000, 1.000000000000000000 ) ) ;
#15604=VERTEX_POINT ( 'NONE', #15400 ) ;
#15608=DIRECTION ( 'NONE',  ( -1.000000000000000000, 0.000000000000000000, -0.000000000000000000 ) ) ;
#15612=DIRECTION ( 'NONE',  ( 0.000000000000000000, 0.000000000000000000, -1.000000000000000000 ) ) ;
#15616=CARTESIAN_POINT ( 'NONE',  ( -23.00000000000002487, 10.00000000000000000, -36.99999999999999289 ) ) ;
#15633=CARTESIAN_POINT ( 'NONE',  ( 21.99999999999998224, 10.00000000000000000, -35.99999999999999289 ) ) ;
#15634=ORIENTED_EDGE ( 'NONE', *, *, #5247, .T. ) ;
#15649=EDGE_CURVE ( 'NONE', #15290, #5055, #4836, .T. ) ;
#15653=CARTESIAN_POINT ( 'NONE',  ( -37.00000000000000711, 6.000000000000000000, 23.00000000000000000 ) ) ;
#15654=ORIENTED_EDGE ( 'NONE', *, *, #12363, .F. ) ;
#15655=VECTOR ( 'NONE', #2964, 1000.000000000000000 ) ;
#15670=CARTESIAN_POINT ( 'NONE',  ( -40.00000000000000711, 10.00000000000000000, -26.00000000000000000 ) ) ;
#15674=DIRECTION ( 'NONE',  ( -0.000000000000000000, -1.000000000000000000, -0.000000000000000000 ) ) ;
#15678=ORIENTED_EDGE ( 'NONE', *, *, #15377, .F. ) ;
#15679=EDGE_CURVE ( 'NONE', #8810, #10067, #8879, .T. ) ;
#15693=CARTESIAN_POINT ( 'NONE',  ( 35.99999999999999289, 8.000000000000000000, 21.99999999999999645 ) ) ;
#15710=PLANE ( 'NONE',  #5539 ) ;
#15715=LINE ( 'NONE', #3964, #3032 ) ;
#15716=EDGE_LOOP ( 'NONE', ( #10077, #13935, #10162, #4371, #15956, #6707 ) ) ;
#15719=LINE ( 'NONE', #9115, #16070 ) ;
#15742=DIRECTION ( 'NONE',  ( 0.000000000000000000, 0.000000000000000000, -1.000000000000000000 ) ) ;
#15743=ORIENTED_EDGE ( 'NONE', *, *, #7823, .F. ) ;
#15750=LINE ( 'NONE', #3998, #9771 ) ;
#15752=ORIENTED_EDGE ( 'NONE', *, *, #7997, .T. ) ;
#15762=CARTESIAN_POINT ( 'NONE',  ( -22.00000000000001776, 6.000000000000000000, 36.00000000000000711 ) ) ;
#15765=CARTESIAN_POINT ( 'NONE',  ( 31.00000000000003553, 0.000000000000000000, -22.99999999999999645 ) ) ;
#15777=ORIENTED_EDGE ( 'NONE', *, *, #8895, .T. ) ;
#15779=CYLINDRICAL_SURFACE ( 'NONE', #11319, 5.000000000000000888 ) ;
#15786=LINE ( 'NONE', #12351, #14581 ) ;
#15800=EDGE_CURVE ( 'NONE', #8348, #2142, #9224, .T. ) ;
#15802=EDGE_CURVE ( 'NONE', #1311, #2938, #4141, .T. ) ;
#15807=AXIS2_PLACEMENT_3D ( 'NONE', #4291, #10712, #14763 ) ;
#15860=VECTOR ( 'NONE', #16894, 1000.000000000000000 ) ;
#15863=PLANE ( 'NONE',  #15807 ) ;
#15866=DIRECTION ( 'NONE',  ( 1.000000000000000000, 0.000000000000000000, 0.000000000000000000 ) ) ;
#15880=DIRECTION ( 'NONE',  ( -1.000000000000000000, 0.000000000000000000, 3.854941057726254367E-16 ) ) ;
#15888=ORIENTED_EDGE ( 'NONE', *, *, #6277, .F. ) ;
#15896=ORIENTED_EDGE ( 'NONE', *, *, #11870, .T. ) ;
#15904=DIRECTION ( 'NONE',  ( -0.000000000000000000, -1.000000000000000000, -0.000000000000000000 ) ) ;
#15934=CARTESIAN_POINT ( 'NONE',  ( 17.99999999999998224, 6.000000000000000000, -35.99999999999999289 ) ) ;
#15956=ORIENTED_EDGE ( 'NONE', *, *, #8483, .T. ) ;
#15969=CARTESIAN_POINT ( 'NONE',  ( -40.00000000000000711, 8.000000000000000000, -19.00000000000000355 ) ) ;
#15982=CARTESIAN_POINT ( 'NONE',  ( 32.99999999999998579, 8.000000000000000000, 21.99999999999999645 ) ) ;
#15989=CARTESIAN_POINT ( 'NONE',  ( -18.00000000000001421, 6.000000000000000000, 37.00000000000000711 ) ) ;
#15998=AXIS2_PLACEMENT_3D ( 'NONE', #12407, #16519, #647 ) ;
#16003=VERTEX_POINT ( 'NONE', #12886 ) ;
#16022=EDGE_CURVE ( 'NONE', #3569, #6167, #2322, .T. ) ;
#16044=FACE_OUTER_BOUND ( 'NONE', #7632, .T. ) ;
#16049=PLANE ( 'NONE',  #16638 ) ;
#16070=VECTOR ( 'NONE', #13239, 1000.000000000000000 ) ;
#16080=AXIS2_PLACEMENT_3D ( 'NONE', #16648, #4955, #13045 ) ;
#16085=LINE ( 'NONE', #10936, #2930 ) ;
#16105=VECTOR ( 'NONE', #10420, 1000.000000000000000 ) ;
#16129=DIRECTION ( 'NONE',  ( 0.000000000000000000, -0.000000000000000000, -1.000000000000000000 ) ) ;
#16133=FACE_OUTER_BOUND ( 'NONE', #12564, .T. ) ;
#16135=DIRECTION ( 'NONE',  ( -0.000000000000000000, -1.000000000000000000, -0.000000000000000000 ) ) ;
#16155=ORIENTED_EDGE ( 'NONE', *, *, #3393, .F. ) ;
#16164=ORIENTED_EDGE ( 'NONE', *, *, #16352, .T. ) ;
#16166=LINE ( 'NONE', #1748, #5110 ) ;
#16167=ORIENTED_EDGE ( 'NONE', *, *, #1837, .F. ) ;
#16193=AXIS2_PLACEMENT_3D ( 'NONE', #11685, #8944, #10317 ) ;
#16209=EDGE_LOOP ( 'NONE', ( #14558, #4388, #12823, #10096 ) ) ;
#16222=ORIENTED_EDGE ( 'NONE', *, *, #9811, .F. ) ;
#16226=DIRECTION ( 'NONE',  ( 0.000000000000000000, 1.000000000000000000, 0.000000000000000000 ) ) ;
#16233=EDGE_CURVE ( 'NONE', #9234, #3717, #268, .T. ) ;
#16241=ORIENTED_EDGE ( 'NONE', *, *, #14733, .T. ) ;
#16243=ORIENTED_EDGE ( 'NONE', *, *, #15134, .T. ) ;
#16252=ORIENTED_EDGE ( 'NONE', *, *, #14545, .T. ) ;
#16255=VERTEX_POINT ( 'NONE', #6509 ) ;
#16260=DIRECTION ( 'NONE',  ( -0.000000000000000000, -1.000000000000000000, 0.000000000000000000 ) ) ;
#16267=ORIENTED_EDGE ( 'NONE', *, *, #9008, .T. ) ;
#16269=EDGE_CURVE ( 'NONE', #5545, #8924, #2745, .T. ) ;
#16277=LINE ( 'NONE', #13867, #15184 ) ;
#16285=CARTESIAN_POINT ( 'NONE',  ( 17.99999999999998224, 10.00000000000000000, -35.99999999999999289 ) ) ;
#16288=ORIENTED_EDGE ( 'NONE', *, *, #9515, .T. ) ;
#16314=DIRECTION ( 'NONE',  ( 1.000000000000000000, 0.000000000000000000, 0.000000000000000000 ) ) ;
#16318=LINE ( 'NONE', #4550, #5556 ) ;
#16332=EDGE_CURVE ( 'NONE', #16779, #14988, #8816, .T. ) ;
#16352=EDGE_CURVE ( 'NONE', #8801, #8170, #14072, .T. ) ;
#16358=FACE_OUTER_BOUND ( 'NONE', #4067, .T. ) ;
#16363=DIRECTION ( 'NONE',  ( -1.000000000000000000, 0.000000000000000000, 4.956352788505159323E-16 ) ) ;
#16365=LINE ( 'NONE', #4597, #2657 ) ;
#16366=PLANE ( 'NONE',  #8026 ) ;
#16368=DIRECTION ( 'NONE',  ( -0.000000000000000000, -1.000000000000000000, -0.000000000000000000 ) ) ;
#16379=ORIENTED_EDGE ( 'NONE', *, *, #16332, .T. ) ;
#16386=VECTOR ( 'NONE', #5135, 1000.000000000000000 ) ;
#16388=LINE ( 'NONE', #593, #14762 ) ;
#16396=FACE_OUTER_BOUND ( 'NONE', #1758, .T. ) ;
#16412=CARTESIAN_POINT ( 'NONE',  ( 25.99999999999998224, 10.00000000000000000, -31.00000000000003197 ) ) ;
#16416=DIRECTION ( 'NONE',  ( 0.000000000000000000, 0.000000000000000000, -1.000000000000000000 ) ) ;
#16424=ORIENTED_EDGE ( 'NONE', *, *, #10168, .T. ) ;
#16429=ORIENTED_EDGE ( 'NONE', *, *, #5116, .F. ) ;
#16431=CARTESIAN_POINT ( 'NONE',  ( -22.00000000000001776, 10.00000000000000000, 32.00000000000000711 ) ) ;
#16437=CARTESIAN_POINT ( 'NONE',  ( -40.00000000000000711, 8.000000000000000000, -19.00000000000000355 ) ) ;
#16444=ADVANCED_FACE ( 'NONE', ( #8569 ), #9066, .F. ) ;
#16453=LINE ( 'NONE', #15082, #1678 ) ;
#16458=DIRECTION ( 'NONE',  ( 0.000000000000000000, -1.000000000000000000, 0.000000000000000000 ) ) ;
#16476=CARTESIAN_POINT ( 'NONE',  ( -31.00000000000001776, 10.00000000000000000, 31.00000000000000000 ) ) ;
#16494=ORIENTED_EDGE ( 'NONE', *, *, #12028, .T. ) ;
#16501=VERTEX_POINT ( 'NONE', #14303 ) ;
#16504=VERTEX_POINT ( 'NONE', #1166 ) ;
#16505=AXIS2_PLACEMENT_3D ( 'NONE', #12160, #7071, #6901 ) ;
#16508=VECTOR ( 'NONE', #12168, 1000.000000000000000 ) ;
#16511=ORIENTED_EDGE ( 'NONE', *, *, #8704, .T. ) ;
#16517=CARTESIAN_POINT ( 'NONE',  ( 22.99999999999998224, 10.00000000000000000, -31.00000000000003197 ) ) ;
#16519=DIRECTION ( 'NONE',  ( -0.000000000000000000, -1.000000000000000000, 0.000000000000000000 ) ) ;
#16522=VECTOR ( 'NONE', #5745, 1000.000000000000000 ) ;
#16523=EDGE_LOOP ( 'NONE', ( #13079, #2333, #2542, #3688 ) ) ;
#16525=FACE_OUTER_BOUND ( 'NONE', #630, .T. ) ;
#16528=ORIENTED_EDGE ( 'NONE', *, *, #7089, .T. ) ;
#16529=AXIS2_PLACEMENT_3D ( 'NONE', #15361, #7616, #14323 ) ;
#16533=CARTESIAN_POINT ( 'NONE',  ( 25.99999999999997868, 0.000000000000000000, -39.99999999999999289 ) ) ;
#16547=FACE_OUTER_BOUND ( 'NONE', #15056, .T. ) ;
#16551=PLANE ( 'NONE',  #13285 ) ;
#16559=ADVANCED_FACE ( 'NONE', ( #7938 ), #5112, .F. ) ;
#16566=VERTEX_POINT ( 'NONE', #15425 ) ;
#16572=VECTOR ( 'NONE', #11324, 1000.000000000000000 ) ;
#16583=( NAMED_UNIT ( * ) PLANE_ANGLE_UNIT ( ) SI_UNIT ( $, .RADIAN. ) );
#16587=LINE ( 'NONE', #16412, #4970 ) ;
#16602=DIRECTION ( 'NONE',  ( -1.000000000000000000, 0.000000000000000000, -1.734723475976807094E-15 ) ) ;
#16606=DIRECTION ( 'NONE',  ( 3.854941057726249930E-16, 0.000000000000000000, 1.000000000000000000 ) ) ;
#16614=AXIS2_PLACEMENT_3D ( 'NONE', #4980, #16914, #4049 ) ;
#16626=ORIENTED_EDGE ( 'NONE', *, *, #11717, .T. ) ;
#16630=EDGE_CURVE ( 'NONE', #5706, #7594, #5016, .T. ) ;
#16635=DIRECTION ( 'NONE',  ( -0.000000000000000000, -1.000000000000000000, -0.000000000000000000 ) ) ;
#16638=AXIS2_PLACEMENT_3D ( 'NONE', #4197, #5468, #14767 ) ;
#16642=EDGE_CURVE ( 'NONE', #14988, #594, #488, .T. ) ;
#16648=CARTESIAN_POINT ( 'NONE',  ( -40.00000000000000711, 10.00000000000000000, 26.00000000000000000 ) ) ;
#16664=ORIENTED_EDGE ( 'NONE', *, *, #15292, .F. ) ;
#16676=ORIENTED_EDGE ( 'NONE', *, *, #9940, .F. ) ;
#16679=DIRECTION ( 'NONE',  ( -0.000000000000000000, -1.000000000000000000, -0.000000000000000000 ) ) ;
#16686=ORIENTED_EDGE ( 'NONE', *, *, #7826, .F. ) ;
#16693=ORIENTED_EDGE ( 'NONE', *, *, #6201, .T. ) ;
#16705=CARTESIAN_POINT ( 'NONE',  ( 30.99999999999997513, 0.000000000000000000, 30.99999999999999645 ) ) ;
#16706=ORIENTED_EDGE ( 'NONE', *, *, #15499, .F. ) ;
#16713=ORIENTED_EDGE ( 'NONE', *, *, #15499, .T. ) ;
#16723=CARTESIAN_POINT ( 'NONE',  ( 31.99999999999998579, 10.00000000000000000, 25.99999999999999645 ) ) ;
#16745=EDGE_CURVE ( 'NONE', #7960, #3043, #16277, .T. ) ;
#16753=ORIENTED_EDGE ( 'NONE', *, *, #11684, .F. ) ;
#16759=ORIENTED_EDGE ( 'NONE', *, *, #782, .T. ) ;
#16763=CARTESIAN_POINT ( 'NONE',  ( 18.99999999999998224, 10.00000000000000000, -39.99999999999999289 ) ) ;
#16764=ADVANCED_FACE ( 'NONE', ( #8461 ), #4516, .F. ) ;
#16767=LINE ( 'NONE', #5002, #3549 ) ;
#16769=EDGE_LOOP ( 'NONE', ( #12392, #757, #13349, #3200, #4972 ) ) ;
#16770=CARTESIAN_POINT ( 'NONE',  ( -31.00000000000007105, 10.00000000000000000, 23.00000000000000000 ) ) ;
#16776=ORIENTED_EDGE ( 'NONE', *, *, #3803, .F. ) ;
#16779=VERTEX_POINT ( 'NONE', #4593 ) ;
#16782=( NAMED_UNIT ( * ) SI_UNIT ( $, .STERADIAN. ) SOLID_ANGLE_UNIT ( ) );
#16783=PLANE ( 'NONE',  #8813 ) ;
#16788=CARTESIAN_POINT ( 'NONE',  ( -26.00000000000002132, 10.00000000000000000, 40.00000000000000711 ) ) ;
#16790=DIRECTION ( 'NONE',  ( -1.000000000000000000, 0.000000000000000000, -0.000000000000000000 ) ) ;
#16800=PLANE ( 'NONE',  #8593 ) ;
#16803=CARTESIAN_POINT ( 'NONE',  ( -33.00000000000000000, 10.00000000000000000, -22.00000000000000355 ) ) ;
#16809=FACE_OUTER_BOUND ( 'NONE', #3519, .T. ) ;
#16811=DIRECTION ( 'NONE',  ( 0.000000000000000000, 1.000000000000000000, 0.000000000000000000 ) ) ;
#16812=ADVANCED_FACE ( 'NONE', ( #12577 ), #2177, .F. ) ;
#16814=CARTESIAN_POINT ( 'NONE',  ( 36.99999999999999289, 10.00000000000000000, 22.99999999999999645 ) ) ;
#16816=ORIENTED_EDGE ( 'NONE', *, *, #14479, .T. ) ;
#16845=EDGE_CURVE ( 'NONE', #16912, #7189, #3476, .T. ) ;
#16848=ORIENTED_EDGE ( 'NONE', *, *, #14231, .F. ) ;
#16855=AXIS2_PLACEMENT_3D ( 'NONE', #2458, #2543, #1176 ) ;
#16856=DIRECTION ( 'NONE',  ( -3.854941057726249437E-16, -0.000000000000000000, 1.000000000000000000 ) ) ;
#16865=EDGE_CURVE ( 'NONE', #6188, #352, #11338, .T. ) ;
#16866=LINE ( 'NONE', #3570, #4819 ) ;
#16872=DIRECTION ( 'NONE',  ( -1.000000000000000000, 0.000000000000000000, 0.000000000000000000 ) ) ;
#16873=ORIENTED_EDGE ( 'NONE', *, *, #16745, .F. ) ;
#16876=DIRECTION ( 'NONE',  ( 0.000000000000000000, 0.000000000000000000, -1.000000000000000000 ) ) ;
#16879=DIRECTION ( 'NONE',  ( 8.673617379884027583E-16, 0.000000000000000000, -1.000000000000000000 ) ) ;
#16888=DIRECTION ( 'NONE',  ( 0.000000000000000000, 0.000000000000000000, 1.000000000000000000 ) ) ;
#16890=DIRECTION ( 'NONE',  ( -0.000000000000000000, -1.000000000000000000, 0.000000000000000000 ) ) ;
#16894=DIRECTION ( 'NONE',  ( -1.000000000000000000, 0.000000000000000000, 0.000000000000000000 ) ) ;
#16911=DIRECTION ( 'NONE',  ( -1.156482317317881191E-15, 0.000000000000000000, -1.000000000000000000 ) ) ;
#16912=VERTEX_POINT ( 'NONE', #8637 ) ;
#16914=DIRECTION ( 'NONE',  ( -0.000000000000000000, 1.000000000000000000, -0.000000000000000000 ) ) ;
#16922=ORIENTED_EDGE ( 'NONE', *, *, #8848, .T. ) ;
#16930=EDGE_LOOP ( 'NONE', ( #5721, #9775, #3105, #2641 ) ) ;
#16931=CARTESIAN_POINT ( 'NONE',  ( -26.00000000000002132, 0.000000000000000000, 40.00000000000000711 ) ) ;
#16938=LINE ( 'NONE', #10348, #4324 ) ;
#16944=VECTOR ( 'NONE', #7404, 1000.000000000000000 ) ;
#16956=EDGE_CURVE ( 'NONE', #2103, #9177, #6199, .T. ) ;
#16957=PLANE ( 'NONE',  #5760 ) ;
ENDSEC;
END-ISO-10303-21;
